ISO-10303-21;
HEADER;
FILE_DESCRIPTION (('STEP AP214'),
    '1' );
FILE_NAME ('cover for positive.step',
    '2026-10-05T20:10:51',
    ( '' ),
    ( '' ),
    'SwSTEP 2.0',
    'SolidWorks 2020',
    '' );
FILE_SCHEMA (( 'AUTOMOTIVE_DESIGN' ));
ENDSEC;

DATA;
#12=CYLINDRICAL_SURFACE ( 'NONE', #60912, 0.5000000000000000000 ) ;
#21=MECHANICAL_DESIGN_GEOMETRIC_PRESENTATION_REPRESENTATION('',(#3437),#103815);
#527=PRODUCT_DEFINITION_CONTEXT ( 'detailed design', #188883, 'design' ) ;
#592=SURFACE_STYLE_USAGE ( .BOTH. , #183645 ) ;
#641=CARTESIAN_POINT ( 'NONE',  ( -1.237941840313982578, -1.374772708486751593, 1.500000000000001332 ) ) ;
#668=ORIENTED_EDGE ( 'NONE', *, *, #118767, .F. ) ;
#739=CARTESIAN_POINT ( 'NONE',  ( 1.790313668900414878, -0.4735605917218765892, 0.7140520948302738757 ) ) ;
#771=DIRECTION ( 'NONE',  ( 8.638326563840814399E-31, -0.000000000000000000, 1.000000000000000000 ) ) ;
#811=CIRCLE ( 'NONE', #45881, 2.725000000000000089 ) ;
#919=DIRECTION ( 'NONE',  ( 8.638326563840814399E-31, 0.000000000000000000, 1.000000000000000000 ) ) ;
#980=VECTOR ( 'NONE', #108007, 1000.000000000000000 ) ;
#1255=DIRECTION ( 'NONE',  ( 0.000000000000000000, 0.000000000000000000, -1.000000000000000000 ) ) ;
#1260=CARTESIAN_POINT ( 'NONE',  ( -1.777638883463123598, -0.9165151389911724289, 1.199999999999999734 ) ) ;
#1560=CYLINDRICAL_SURFACE ( 'NONE', #93873, 0.4000000000000010214 ) ;
#1779=EDGE_LOOP ( 'NONE', ( #104681, #212819 ) ) ;
#2139=( NAMED_UNIT ( * ) SI_UNIT ( $, .STERADIAN. ) SOLID_ANGLE_UNIT ( ) );
#2218=ORIENTED_EDGE ( 'NONE', *, *, #126729, .T. ) ;
#2242=ORIENTED_EDGE ( 'NONE', *, *, #150221, .T. ) ;
#2271=CARTESIAN_POINT ( 'NONE',  ( 2.671705178897700428, 0.4353224022266768967, -0.1180795802420642887 ) ) ;
#2410=CARTESIAN_POINT ( 'NONE',  ( 0.000000000000000000, 0.000000000000000000, -0.5000000000000004441 ) ) ;
#2498=DIRECTION ( 'NONE',  ( -8.638326563840814399E-31, 0.000000000000000000, -1.000000000000000000 ) ) ;
#3149=DIRECTION ( 'NONE',  ( 8.638326563840809144E-31, 5.962633348652903386E-61, -1.000000000000000000 ) ) ;
#3254=VERTEX_POINT ( 'NONE', #57848 ) ;
#3437=STYLED_ITEM ( 'NONE', ( #132805 ), #122417 ) ;
#3679=CARTESIAN_POINT ( 'NONE',  ( 2.580963302752299349, -0.4788041664876945269, 0.000000000000000000 ) ) ;
#4444=CARTESIAN_POINT ( 'NONE',  ( -1.628336349302364372, -1.162346226930493387, 1.455206426644551243 ) ) ;
#4447=VERTEX_POINT ( 'NONE', #54637 ) ;
#4529=DIRECTION ( 'NONE',  ( 1.000000000000000000, 1.725633230170963762E-31, 8.638326563840814399E-31 ) ) ;
#4722=( NAMED_UNIT ( * ) SI_UNIT ( $, .STERADIAN. ) SOLID_ANGLE_UNIT ( ) );
#4776=CARTESIAN_POINT ( 'NONE',  ( -1.607015867998815128, 0.9165151389911810886, 1.199999999999999734 ) ) ;
#4927=EDGE_CURVE ( 'NONE', #71186, #103536, #77988, .T. ) ;
#5211=MECHANICAL_DESIGN_GEOMETRIC_PRESENTATION_REPRESENTATION('',(#64005),#147052);
#5322=EDGE_LOOP ( 'NONE', ( #668, #88355, #119854, #35076 ) ) ;
#5360=ORIENTED_EDGE ( 'NONE', *, *, #184823, .T. ) ;
#5366=EDGE_CURVE ( 'NONE', #10766, #101960, #196600, .T. ) ;
#5437=DIRECTION ( 'NONE',  ( 8.638326563840814399E-31, 0.000000000000000000, 1.000000000000000000 ) ) ;
#5553=CARTESIAN_POINT ( 'NONE',  ( -1.734935157289736685, -1.374772708486751593, 1.500000000000001332 ) ) ;
#5644=CARTESIAN_POINT ( 'NONE',  ( -2.675383846940428967, -0.4458684588859937459, -0.1127173061977598811 ) ) ;
#5768=EDGE_CURVE ( 'NONE', #191630, #187511, #12121, .T. ) ;
#6073=ORIENTED_EDGE ( 'NONE', *, *, #164541, .T. ) ;
#6214=EDGE_CURVE ( 'NONE', #103536, #133104, #63815, .T. ) ;
#6278=AXIS2_PLACEMENT_3D ( 'NONE', #155863, #25839, #24775 ) ;
#6395=CARTESIAN_POINT ( 'NONE',  ( 0.000000000000000000, 0.000000000000000000, 0.000000000000000000 ) ) ;
#6420=ORIENTED_EDGE ( 'NONE', *, *, #182196, .T. ) ;
#7077=CARTESIAN_POINT ( 'NONE',  ( -1.999999999999988010, 2.428614679364265457E-14, 0.5999999999999969802 ) ) ;
#7184=DIRECTION ( 'NONE',  ( 8.638326563840814399E-31, -0.000000000000000000, 1.000000000000000000 ) ) ;
#7294=AXIS2_PLACEMENT_3D ( 'NONE', #13753, #192501, #191433 ) ;
#7315=ADVANCED_FACE ( 'NONE', ( #180925 ), #12, .T. ) ;
#7329=ORIENTED_EDGE ( 'NONE', *, *, #102584, .T. ) ;
#7974=CIRCLE ( 'NONE', #32258, 0.09999999999999982514 ) ;
#8278=ORIENTED_EDGE ( 'NONE', *, *, #199264, .F. ) ;
#8333=DIRECTION ( 'NONE',  ( -1.000000000000000000, -1.725633230170963762E-31, -8.638326563840814399E-31 ) ) ;
#8504=LINE ( 'NONE', #60453, #143679 ) ;
#8529=FACE_OUTER_BOUND ( 'NONE', #166307, .T. ) ;
#8574=CARTESIAN_POINT ( 'NONE',  ( -5.249999999999987566, 1.374772708486751593, 1.000000000000000888 ) ) ;
#8956=CIRCLE ( 'NONE', #115848, 0.09999999999999982514 ) ;
#9051=CARTESIAN_POINT ( 'NONE',  ( 1.815167269671989603, 0.3943365573011955449, 0.6613654005181966999 ) ) ;
#9350=CARTESIAN_POINT ( 'NONE',  ( 0.000000000000000000, 0.000000000000000000, 0.000000000000000000 ) ) ;
#9388=ORIENTED_EDGE ( 'NONE', *, *, #127726, .F. ) ;
#9422=CARTESIAN_POINT ( 'NONE',  ( 2.325000000000005063, -1.380506584136773637E-31, 3.455330625536333992E-31 ) ) ;
#9722=EDGE_CURVE ( 'NONE', #171541, #162523, #121062, .T. ) ;
#9731=LINE ( 'NONE', #193810, #64732 ) ;
#9985=CARTESIAN_POINT ( 'NONE',  ( 2.680951471028992117, -0.4698187958462032299, -0.1032074697909405592 ) ) ;
#10017=DIRECTION ( 'NONE',  ( 8.638326563840814399E-31, 0.000000000000000000, 1.000000000000000000 ) ) ;
#10112=VERTEX_POINT ( 'NONE', #123154 ) ;
#10399=CARTESIAN_POINT ( 'NONE',  ( 1.734935157289751562, 1.374772708486753370, 1.500000000000001332 ) ) ;
#10430=ORIENTED_EDGE ( 'NONE', *, *, #30893, .F. ) ;
#10766=VERTEX_POINT ( 'NONE', #163566 ) ;
#10899=CARTESIAN_POINT ( 'NONE',  ( -1.607015867998808023, -0.9165151389911689872, 1.199999999999999734 ) ) ;
#11115=DIRECTION ( 'NONE',  ( 8.638326563840814399E-31, 0.000000000000000000, 1.000000000000000000 ) ) ;
#11468=CYLINDRICAL_SURFACE ( 'NONE', #175789, 1.000000000000000222 ) ;
#11595=CARTESIAN_POINT ( 'NONE',  ( 2.000000000000000000, 2.453105802350469389E-14, -1.733336949948507013E-30 ) ) ;
#11736=DIRECTION ( 'NONE',  ( 1.000000000000000000, 0.000000000000000000, 0.000000000000000000 ) ) ;
#11892=AXIS2_PLACEMENT_3D ( 'NONE', #211954, #199964, #198888 ) ;
#12116=CARTESIAN_POINT ( 'NONE',  ( 2.677589438261873234, -0.4530478092824203884, -0.1093532045961659316 ) ) ;
#12121=CIRCLE ( 'NONE', #19073, 0.4000000000000010214 ) ;
#12299=DIRECTION ( 'NONE',  ( -8.638326563840809144E-31, -5.962633348652903386E-61, 1.000000000000000000 ) ) ;
#12586=ORIENTED_EDGE ( 'NONE', *, *, #179634, .T. ) ;
#12704=DIRECTION ( 'NONE',  ( 1.000000000000000000, 1.725633230170963762E-31, 8.638326563840814399E-31 ) ) ;
#12718=( GEOMETRIC_REPRESENTATION_CONTEXT ( 3 ) GLOBAL_UNCERTAINTY_ASSIGNED_CONTEXT ( ( #81898 ) ) GLOBAL_UNIT_ASSIGNED_CONTEXT ( ( #108750, #88165, #193124 ) ) REPRESENTATION_CONTEXT ( 'NONE', 'WORKASPACE' ) );
#13095=AXIS2_PLACEMENT_3D ( 'NONE', #34513, #919, #49703 ) ;
#13139=CARTESIAN_POINT ( 'NONE',  ( -2.609770642201835855, -0.3830433331901521576, -0.1872689674646474400 ) ) ;
#13189=EDGE_LOOP ( 'NONE', ( #126180, #83708, #68325, #174794 ) ) ;
#13574=CARTESIAN_POINT ( 'NONE',  ( -2.609770642201835855, 0.3830433331901555993, -0.1872689674646474400 ) ) ;
#13753=CARTESIAN_POINT ( 'NONE',  ( 0.000000000000000000, 0.000000000000000000, -5.732590180780448463 ) ) ;
#14189=CARTESIAN_POINT ( 'NONE',  ( -2.624193383061824036, -0.3882907696143628185, -0.1722368472184268029 ) ) ;
#14628=CARTESIAN_POINT ( 'NONE',  ( -2.680963273416246295, 0.4787157238462547704, -0.1016320821874245467 ) ) ;
#14717=EDGE_LOOP ( 'NONE', ( #163470, #70457, #115751, #36232, #7329 ) ) ;
#14920=CARTESIAN_POINT ( 'NONE',  ( 2.540289672789934450, 0.3621416576072679083, -0.2590487051680201436 ) ) ;
#15498=VERTEX_POINT ( 'NONE', #124213 ) ;
#15590=COLOUR_RGB ( '', 0.08235294, 0.09019608, 0.10196078) ;
#15708=CARTESIAN_POINT ( 'NONE',  ( 1.754755943840834664, -0.9608980427861594231, 1.301694008101298428 ) ) ;
#16267=SURFACE_STYLE_USAGE ( .BOTH. , #164683 ) ;
#16330=LINE ( 'NONE', #35796, #75197 ) ;
#16444=CARTESIAN_POINT ( 'NONE',  ( 2.335253425310769071, -0.1017894593877440301, -0.4879271257269311990 ) ) ;
#16740=ORIENTED_EDGE ( 'NONE', *, *, #109311, .T. ) ;
#16748=ADVANCED_FACE ( 'NONE', ( #174774 ), #24203, .T. ) ;
#16863=FILL_AREA_STYLE ('',( #165268 ) ) ;
#16952=DIRECTION ( 'NONE',  ( -8.638326563840814399E-31, 0.000000000000000000, -1.000000000000000000 ) ) ;
#17007=CARTESIAN_POINT ( 'NONE',  ( 1.715338164143669353, -0.7127732114542313369, 0.8729459113246081925 ) ) ;
#17030=ORIENTED_EDGE ( 'NONE', *, *, #147441, .T. ) ;
#17311=CARTESIAN_POINT ( 'NONE',  ( 1.237941840314000785, -1.374772708486730943, 1.500000000000001332 ) ) ;
#17464=CARTESIAN_POINT ( 'NONE',  ( 2.617062827300069117, 0.3852370113777958682, -0.1797355214283801461 ) ) ;
#17487=CARTESIAN_POINT ( 'NONE',  ( 2.679285714285720044, -0.4970443252110337551, -0.09999999999999592548 ) ) ;
#17510=EDGE_CURVE ( 'NONE', #106638, #92178, #25033, .T. ) ;
#17923=( NAMED_UNIT ( * ) SI_UNIT ( $, .STERADIAN. ) SOLID_ANGLE_UNIT ( ) );
#18018=DIRECTION ( 'NONE',  ( -1.000000000000000000, -3.451266460341925773E-31, -8.638326563840809144E-31 ) ) ;
#18383=EDGE_CURVE ( 'NONE', #25559, #122127, #16330, .T. ) ;
#18439=EDGE_LOOP ( 'NONE', ( #45940, #191936, #63009, #118299 ) ) ;
#18493=AXIS2_PLACEMENT_3D ( 'NONE', #159435, #40374, #173591 ) ;
#18586=CARTESIAN_POINT ( 'NONE',  ( 2.393657244693859543, -0.2279079664470242961, -0.4206872822309609128 ) ) ;
#18787=AXIS2_PLACEMENT_3D ( 'NONE', #2410, #169209, #70611 ) ;
#18915=CARTESIAN_POINT ( 'NONE',  ( -1.850000000000000089, 2.265195232789710231E-16, 0.5999999999999969802 ) ) ;
#19073=AXIS2_PLACEMENT_3D ( 'NONE', #123548, #92046, #174360 ) ;
#19556=AXIS2_PLACEMENT_3D ( 'NONE', #8574, #207834, #26951 ) ;
#19654=CARTESIAN_POINT ( 'NONE',  ( 2.325000000000005507, -0.05106137233530404218, -0.4999999999999945044 ) ) ;
#20439=B_SPLINE_CURVE_WITH_KNOTS ( 'NONE', 3,
 ( #22973, #38190, #138907, #186562, #88006, #73891, #5644, #89091, #155145, #24053, #79215, #59766, #76020, #14189, #195105, #13139 ),
 .UNSPECIFIED., .F., .F.,
 ( 4, 3, 3, 3, 3, 4 ),
 ( 0.000000000000000000, 2.688023894042651662E-05, 5.355394816896161286E-05, 9.073944566322023530E-05, 0.0001419156937261415808, 0.0001738851243175521086 ),
 .UNSPECIFIED. ) ;
#20638=LINE ( 'NONE', #51035, #128922 ) ;
#20665=CARTESIAN_POINT ( 'NONE',  ( 2.680843577923686105, 0.4731804818897447640, -0.1027188127693821618 ) ) ;
#20792=( LENGTH_UNIT ( ) NAMED_UNIT ( * ) SI_UNIT ( .MILLI., .METRE. ) );
#20980=CARTESIAN_POINT ( 'NONE',  ( 1.817809523595309340, 0.8386016503486221074, 1.021477770318707234 ) ) ;
#20998=ORIENTED_EDGE ( 'NONE', *, *, #188915, .T. ) ;
#21453=DIRECTION ( 'NONE',  ( -8.638326563840814399E-31, 0.000000000000000000, -1.000000000000000000 ) ) ;
#21565=DIRECTION ( 'NONE',  ( -8.638326563840814399E-31, 0.000000000000000000, -1.000000000000000000 ) ) ;
#21582=DIRECTION ( 'NONE',  ( 0.000000000000000000, 0.000000000000000000, -1.000000000000000000 ) ) ;
#21689=DIRECTION ( 'NONE',  ( 1.000000000000000000, 1.725633230170963762E-31, 8.638326563840814399E-31 ) ) ;
#21745=DIRECTION ( 'NONE',  ( -8.638326563840814399E-31, 0.000000000000000000, -1.000000000000000000 ) ) ;
#21757=CARTESIAN_POINT ( 'NONE',  ( -1.530148271428807716, 1.292818251517726447, 1.500000000002693623 ) ) ;
#21806=DIRECTION ( 'NONE',  ( -1.000000000000000000, -3.451266460341926649E-31, -8.638326563840809144E-31 ) ) ;
#21887=CARTESIAN_POINT ( 'NONE',  ( -2.609770642201835855, -0.3830433331901521576, -0.1872689674646474400 ) ) ;
#22040=PRESENTATION_STYLE_ASSIGNMENT (( #57781 ) ) ;
#22177=( NAMED_UNIT ( * ) SI_UNIT ( $, .STERADIAN. ) SOLID_ANGLE_UNIT ( ) );
#22300=B_SPLINE_CURVE_WITH_KNOTS ( 'NONE', 3,
 ( #69457, #135562, #71589, #153940, #4444, #203718, #120443, #156075 ),
 .UNSPECIFIED., .F., .F.,
 ( 4, 2, 2, 4 ),
 ( 0.000000000000000000, 0.0001671579969091580335, 0.0003343159938183160669, 0.0006686319876366318086 ),
 .UNSPECIFIED. ) ;
#22973=CARTESIAN_POINT ( 'NONE',  ( -2.679285714285713826, -0.4970443252110337551, -0.09999999999999592548 ) ) ;
#23140=DIRECTION ( 'NONE',  ( -8.638326563840814399E-31, 0.000000000000000000, -1.000000000000000000 ) ) ;
#23141=CIRCLE ( 'NONE', #203114, 0.09999999999999982514 ) ;
#24053=CARTESIAN_POINT ( 'NONE',  ( -2.660307654469991068, -0.4179397774614554417, -0.1320628536826823352 ) ) ;
#24099=EDGE_LOOP ( 'NONE', ( #66148, #68249, #133847, #191907 ) ) ;
#24203=CYLINDRICAL_SURFACE ( 'NONE', #106174, 0.5000000000000000000 ) ;
#24356=CARTESIAN_POINT ( 'NONE',  ( -2.580963302752292243, 0.4788041664876945269, 0.000000000000000000 ) ) ;
#24775=DIRECTION ( 'NONE',  ( 1.000000000000000000, 3.451266460341926211E-31, 0.000000000000000000 ) ) ;
#25033=LINE ( 'NONE', #5553, #206451 ) ;
#25171=LINE ( 'NONE', #91272, #80701 ) ;
#25287=SURFACE_SIDE_STYLE ('',( #120743 ) ) ;
#25559=VERTEX_POINT ( 'NONE', #49498 ) ;
#25584=LINE ( 'NONE', #10399, #82369 ) ;
#25736=( GEOMETRIC_REPRESENTATION_CONTEXT ( 3 ) GLOBAL_UNCERTAINTY_ASSIGNED_CONTEXT ( ( #79765 ) ) GLOBAL_UNIT_ASSIGNED_CONTEXT ( ( #187316, #184111, #2139 ) ) REPRESENTATION_CONTEXT ( 'NONE', 'WORKASPACE' ) );
#25755=AXIS2_PLACEMENT_3D ( 'NONE', #134614, #68487, #171339 ) ;
#25764=LINE ( 'NONE', #124437, #120535 ) ;
#25839=DIRECTION ( 'NONE',  ( 8.638326563840814399E-31, 0.000000000000000000, 1.000000000000000000 ) ) ;
#25884=FILL_AREA_STYLE_COLOUR ( '', #26525 ) ;
#25951=CARTESIAN_POINT ( 'NONE',  ( -2.580963302752292243, 0.4788041664876945269, 0.000000000000000000 ) ) ;
#26015=CARTESIAN_POINT ( 'NONE',  ( -2.680963302752291000, 0.4848410213535060964, -0.1005551520456262199 ) ) ;
#26525=COLOUR_RGB ( '', 0.09019608, 0.27058824, 0.51372549) ;
#26668=DIRECTION ( 'NONE',  ( -8.638326563840814399E-31, 0.000000000000000000, -1.000000000000000000 ) ) ;
#26951=DIRECTION ( 'NONE',  ( 0.000000000000000000, 0.000000000000000000, -1.000000000000000000 ) ) ;
#27041=DIRECTION ( 'NONE',  ( 8.638326563840814399E-31, -0.000000000000000000, 1.000000000000000000 ) ) ;
#27144=CARTESIAN_POINT ( 'NONE',  ( 2.609770642201841184, 0.3830433331901660354, 0.000000000000000000 ) ) ;
#27319=ORIENTED_EDGE ( 'NONE', *, *, #18383, .F. ) ;
#27700=DIRECTION ( 'NONE',  ( 1.000000000000000000, 1.725633230170963762E-31, 8.638326563840814399E-31 ) ) ;
#27889=B_SPLINE_CURVE_WITH_KNOTS ( 'NONE', 3,
 ( #111170, #15708, #78591, #194478, #30935, #46121 ),
 .UNSPECIFIED., .F., .F.,
 ( 4, 2, 4 ),
 ( 0.000000000000000000, 0.0003346294579448533951, 0.0006692589158897067902 ),
 .UNSPECIFIED. ) ;
#27912=EDGE_CURVE ( 'NONE', #194519, #25559, #27889, .T. ) ;
#28125=ORIENTED_EDGE ( 'NONE', *, *, #40765, .F. ) ;
#28534=ORIENTED_EDGE ( 'NONE', *, *, #5768, .T. ) ;
#28953=CARTESIAN_POINT ( 'NONE',  ( -2.370092853298476854, -0.1904551827020759536, -0.4476525039842733644 ) ) ;
#29072=DIRECTION ( 'NONE',  ( 8.638326563840814399E-31, 0.000000000000000000, 1.000000000000000000 ) ) ;
#29158=CARTESIAN_POINT ( 'NONE',  ( -2.474627113408586876, 0.3228523939998627079, -0.3300564308867506291 ) ) ;
#29276=EDGE_CURVE ( 'NONE', #10766, #134057, #811, .T. ) ;
#29471=ORIENTED_EDGE ( 'NONE', *, *, #73420, .T. ) ;
#29573=DIRECTION ( 'NONE',  ( 0.000000000000000000, 0.000000000000000000, -1.000000000000000000 ) ) ;
#29847=LINE ( 'NONE', #197650, #48712 ) ;
#30025=FACE_OUTER_BOUND ( 'NONE', #152812, .T. ) ;
#30609=CARTESIAN_POINT ( 'NONE',  ( -1.999999999999988010, 2.428614679364265457E-14, 0.5999999999999969802 ) ) ;
#30687=ORIENTED_EDGE ( 'NONE', *, *, #40765, .T. ) ;
#30834=CARTESIAN_POINT ( 'NONE',  ( 1.754679937794483280, 0.9610454613041006233, 1.302031786359980181 ) ) ;
#30893=EDGE_CURVE ( 'NONE', #85328, #35153, #171868, .T. ) ;
#30935=CARTESIAN_POINT ( 'NONE',  ( 1.530148271428825923, -1.292818251517693584, 1.500000000002693179 ) ) ;
#31095=VERTEX_POINT ( 'NONE', #140212 ) ;
#31783=DIRECTION ( 'NONE',  ( 1.000000000000000000, 3.451266460341926649E-31, 8.638326563840809144E-31 ) ) ;
#32258=AXIS2_PLACEMENT_3D ( 'NONE', #65654, #115562, #98209 ) ;
#32406=CARTESIAN_POINT ( 'NONE',  ( 1.214306433183764966E-14, 2.428612866367529932E-14, 1.500000000000001332 ) ) ;
#32546=FILL_AREA_STYLE ('',( #99679 ) ) ;
#32557=CARTESIAN_POINT ( 'NONE',  ( -1.817608056788086346, 0.8389924079203545659, 1.022373108394139196 ) ) ;
#32606=ORIENTED_EDGE ( 'NONE', *, *, #189930, .F. ) ;
#32619=VECTOR ( 'NONE', #21453, 1000.000000000000000 ) ;
#32716=CARTESIAN_POINT ( 'NONE',  ( 2.609770642201842072, -0.3830433331901555993, -0.1872689674646474400 ) ) ;
#32949=ORIENTED_EDGE ( 'NONE', *, *, #65677, .T. ) ;
#33031=CARTESIAN_POINT ( 'NONE',  ( 2.725000000000005862, 0.000000000000000000, 0.000000000000000000 ) ) ;
#33078=VECTOR ( 'NONE', #89822, 1000.000000000000000 ) ;
#33363=VECTOR ( 'NONE', #147215, 1000.000000000000000 ) ;
#33463=DIRECTION ( 'NONE',  ( 8.638326563840814399E-31, 0.000000000000000000, 1.000000000000000000 ) ) ;
#33663=VERTEX_POINT ( 'NONE', #151801 ) ;
#33734=CARTESIAN_POINT ( 'NONE',  ( 2.678032581596942130, 0.4534618882029567422, -0.1088563323523697446 ) ) ;
#34337=CARTESIAN_POINT ( 'NONE',  ( 1.607015867998833336, -0.9165151389911481150, 1.199999999999999734 ) ) ;
#34513=CARTESIAN_POINT ( 'NONE',  ( 0.000000000000000000, 0.000000000000000000, -0.5000000000000004441 ) ) ;
#34829=CARTESIAN_POINT ( 'NONE',  ( -1.452583904633382383, 1.374772708486763806, 1.500000000000001332 ) ) ;
#35056=FACE_OUTER_BOUND ( 'NONE', #184614, .T. ) ;
#35076=ORIENTED_EDGE ( 'NONE', *, *, #4927, .T. ) ;
#35140=FACE_OUTER_BOUND ( 'NONE', #66571, .T. ) ;
#35153=VERTEX_POINT ( 'NONE', #27144 ) ;
#35260=SHAPE_DEFINITION_REPRESENTATION ( #145815, #99753 ) ;
#35529=STYLED_ITEM ( 'NONE', ( #141019 ), #177196 ) ;
#35796=CARTESIAN_POINT ( 'NONE',  ( 1.559647396048226220, -1.374772708486730943, 1.500000000000001332 ) ) ;
#35866=CARTESIAN_POINT ( 'NONE',  ( 2.641766398690003292, 0.3984423641809177741, -0.1533590935930815580 ) ) ;
#35905=CARTESIAN_POINT ( 'NONE',  ( -1.777638883463106279, 0.9165151389911794233, 1.199999999999999734 ) ) ;
#35930=CARTESIAN_POINT ( 'NONE',  ( 1.968007779264384194, -0.3930682408332056843, 0.6607764497958503735 ) ) ;
#36048=ORIENTED_EDGE ( 'NONE', *, *, #194299, .T. ) ;
#36212=ORIENTED_EDGE ( 'NONE', *, *, #191584, .F. ) ;
#36232=ORIENTED_EDGE ( 'NONE', *, *, #55163, .T. ) ;
#36656=CARTESIAN_POINT ( 'NONE',  ( -1.607015867998815128, 0.9165151389911810886, 1.199999999999999734 ) ) ;
#36897=CYLINDRICAL_SURFACE ( 'NONE', #116747, 2.725000000000000089 ) ;
#36928=CARTESIAN_POINT ( 'NONE',  ( 2.624193383061829365, 0.3882907696143748644, -0.1722368472184270249 ) ) ;
#36936=EDGE_LOOP ( 'NONE', ( #88507, #156816, #206433, #129327 ) ) ;
#37413=CARTESIAN_POINT ( 'NONE',  ( 2.609770642201842072, -0.3830433331901555993, -0.1872689674646474400 ) ) ;
#37740=LINE ( 'NONE', #154696, #32619 ) ;
#37855=DIRECTION ( 'NONE',  ( -1.000000000000000000, -3.451266460341927087E-31, -8.638326563840810896E-31 ) ) ;
#38190=CARTESIAN_POINT ( 'NONE',  ( -2.680920047035027842, -0.4882345588269855763, -0.09999999999999592548 ) ) ;
#38521=ORIENTED_EDGE ( 'NONE', *, *, #189935, .T. ) ;
#38657=ORIENTED_EDGE ( 'NONE', *, *, #43201, .T. ) ;
#38936=EDGE_LOOP ( 'NONE', ( #126806, #64979, #135951, #92013, #28125, #12586 ) ) ;
#39046=CARTESIAN_POINT ( 'NONE',  ( 0.000000000000000000, 0.000000000000000000, -0.5000000000000004441 ) ) ;
#39085=CARTESIAN_POINT ( 'NONE',  ( -2.680963302752293664, 0.4788041664877169534, -0.1016165050528608921 ) ) ;
#39143=EDGE_CURVE ( 'NONE', #126275, #194519, #25764, .T. ) ;
#39202=( NAMED_UNIT ( * ) PLANE_ANGLE_UNIT ( ) SI_UNIT ( $, .RADIAN. ) );
#39709=CARTESIAN_POINT ( 'NONE',  ( 0.000000000000000000, 0.000000000000000000, -0.09999999999999592548 ) ) ;
#40027=AXIS2_PLACEMENT_3D ( 'NONE', #166428, #16952, #18018 ) ;
#40314=B_SPLINE_CURVE_WITH_KNOTS ( 'NONE', 3,
 ( #1260, #117233, #100911, #167000, #112983, #150758, #178994, #30609 ),
 .UNSPECIFIED., .F., .F.,
 ( 4, 2, 2, 4 ),
 ( 0.0003130156513459784388, 0.0009018580307267097616, 0.001196279220417075613, 0.001490700410107441247 ),
 .UNSPECIFIED. ) ;
#40374=DIRECTION ( 'NONE',  ( 8.638326563840814399E-31, -0.000000000000000000, 1.000000000000000000 ) ) ;
#40480=CARTESIAN_POINT ( 'NONE',  ( 1.965118028437739639, 0.3835514080770347500, 0.6713998180129714388 ) ) ;
#40495=AXIS2_PLACEMENT_3D ( 'NONE', #39709, #7184, #185934 ) ;
#40621=SHAPE_REPRESENTATION_RELATIONSHIP ( 'NONE' , 'NONE' ,  #99753, #122417 ) ;
#40699=LINE ( 'NONE', #73157, #177547 ) ;
#40744=ADVANCED_FACE ( 'NONE', ( #168052 ), #100906, .F. ) ;
#40765=EDGE_CURVE ( 'NONE', #62251, #140937, #89492, .T. ) ;
#40865=CARTESIAN_POINT ( 'NONE',  ( -2.609770642201835855, 0.3830433331901538785, 0.000000000000000000 ) ) ;
#40961=EDGE_CURVE ( 'NONE', #92178, #156117, #22300, .T. ) ;
#41322=ORIENTED_EDGE ( 'NONE', *, *, #201896, .T. ) ;
#41569=FILL_AREA_STYLE ('',( #136925 ) ) ;
#41896=CARTESIAN_POINT ( 'NONE',  ( 2.609770642201841184, 0.3830433331901660354, 0.000000000000000000 ) ) ;
#41935=LINE ( 'NONE', #90682, #178233 ) ;
#42045=VECTOR ( 'NONE', #112957, 1000.000000000000000 ) ;
#42102=ADVANCED_FACE ( 'NONE', ( #206079 ), #76092, .T. ) ;
#42504=AXIS2_PLACEMENT_3D ( 'NONE', #154439, #171745, #72089 ) ;
#42677=EDGE_LOOP ( 'NONE', ( #111729, #182209, #116212, #29471 ) ) ;
#42749=FACE_OUTER_BOUND ( 'NONE', #195568, .T. ) ;
#43089=CARTESIAN_POINT ( 'NONE',  ( -1.777638883463106279, 0.9165151389911794233, 1.199999999999999734 ) ) ;
#43201=EDGE_CURVE ( 'NONE', #152613, #85328, #153925, .T. ) ;
#43241=FILL_AREA_STYLE ('',( #25884 ) ) ;
#43294=ORIENTED_EDGE ( 'NONE', *, *, #199736, .T. ) ;
#43530=ORIENTED_EDGE ( 'NONE', *, *, #73420, .F. ) ;
#44649=CARTESIAN_POINT ( 'NONE',  ( 2.680963214763174118, -0.4786715097226356130, -0.1016399112248461689 ) ) ;
#44684=ADVANCED_FACE ( 'NONE', ( #103039 ), #183212, .T. ) ;
#44689=ORIENTED_EDGE ( 'NONE', *, *, #187563, .F. ) ;
#44708=LINE ( 'NONE', #195206, #42045 ) ;
#45425=CARTESIAN_POINT ( 'NONE',  ( -2.540684401258873848, 0.3622604021566178667, -0.2586409171621191216 ) ) ;
#45633=CARTESIAN_POINT ( 'NONE',  ( -1.968007779264361323, 0.3930682408332470956, 0.6607764497958683592 ) ) ;
#45817=ORIENTED_EDGE ( 'NONE', *, *, #112585, .T. ) ;
#45881=AXIS2_PLACEMENT_3D ( 'NONE', #6395, #21565, #37855 ) ;
#45940=ORIENTED_EDGE ( 'NONE', *, *, #90754, .F. ) ;
#46080=CONICAL_SURFACE ( 'NONE', #111848, 2.324999999999998845, 0.7853981633974461696 ) ;
#46121=CARTESIAN_POINT ( 'NONE',  ( 1.452583904633400591, -1.374772708486727391, 1.500000000000001332 ) ) ;
#46396=CARTESIAN_POINT ( 'NONE',  ( 2.393960638069839941, 0.2282907053230429639, -0.4203461706283275201 ) ) ;
#46427=DIRECTION ( 'NONE',  ( 1.000000000000000000, 1.725633230170963762E-31, 8.638326563840814399E-31 ) ) ;
#46655=EDGE_CURVE ( 'NONE', #122458, #167565, #73298, .T. ) ;
#46659=AXIS2_PLACEMENT_3D ( 'NONE', #175370, #142892, #156987 ) ;
#46787=CARTESIAN_POINT ( 'NONE',  ( 2.680971279526301210, -0.4847509252939742885, -0.1005634232587017118 ) ) ;
#46860=CARTESIAN_POINT ( 'NONE',  ( -1.850000000000000089, 2.265596578422597184E-16, -5.732590180780448463 ) ) ;
#47720=VERTEX_POINT ( 'NONE', #65254 ) ;
#48712=VECTOR ( 'NONE', #27700, 1000.000000000000000 ) ;
#49096=FACE_OUTER_BOUND ( 'NONE', #42677, .T. ) ;
#49498=CARTESIAN_POINT ( 'NONE',  ( 1.452583904633400591, -1.374772708486727391, 1.500000000000001332 ) ) ;
#49518=EDGE_LOOP ( 'NONE', ( #138920, #53703, #196339, #126661 ) ) ;
#49530=CARTESIAN_POINT ( 'NONE',  ( 1.850000000000000311, -0.09855238430051822818, 0.5999999999999969802 ) ) ;
#49703=DIRECTION ( 'NONE',  ( 1.000000000000000000, 3.451266460341926649E-31, 0.000000000000000000 ) ) ;
#49846=CARTESIAN_POINT ( 'NONE',  ( 2.679285714285720044, 0.4970443252110459120, -0.5000000000000004441 ) ) ;
#50522=ORIENTED_EDGE ( 'NONE', *, *, #6214, .F. ) ;
#50534=CIRCLE ( 'NONE', #40027, 0.4000000000000010214 ) ;
#50627=DIRECTION ( 'NONE',  ( -1.000000000000000000, 5.421010862427531636E-15, -8.638326563840826660E-31 ) ) ;
#50676=CIRCLE ( 'NONE', #123304, 1.850000000000000089 ) ;
#50862=EDGE_CURVE ( 'NONE', #148041, #105242, #87253, .T. ) ;
#51035=CARTESIAN_POINT ( 'NONE',  ( -5.249999999999987566, 0.000000000000000000, 0.5999999999999969802 ) ) ;
#51062=CARTESIAN_POINT ( 'NONE',  ( 2.675383846940436072, 0.4458684588860059028, -0.1127173061977529422 ) ) ;
#51130=CARTESIAN_POINT ( 'NONE',  ( 1.817608056788092563, -0.8389924079203456841, 1.022373108394124985 ) ) ;
#51590=EDGE_CURVE ( 'NONE', #10112, #116404, #173667, .T. ) ;
#51771=PRODUCT_DEFINITION ( 'UNKNOWN', '', #163028, #527 ) ;
#52075=VERTEX_POINT ( 'NONE', #7077 ) ;
#52105=ORIENTED_EDGE ( 'NONE', *, *, #199264, .T. ) ;
#52129=CARTESIAN_POINT ( 'NONE',  ( 2.666414593264813337, 0.4259009368094319181, -0.1247943508829645470 ) ) ;
#52194=FACE_OUTER_BOUND ( 'NONE', #183807, .T. ) ;
#52395=CYLINDRICAL_SURFACE ( 'NONE', #171548, 0.09999999999999982514 ) ;
#53271=EDGE_LOOP ( 'NONE', ( #103103, #212461, #64697, #109125 ) ) ;
#53539=CARTESIAN_POINT ( 'NONE',  ( -1.237941840313982578, 1.374772708486763806, 1.500000000000001332 ) ) ;
#53703=ORIENTED_EDGE ( 'NONE', *, *, #179393, .T. ) ;
#54331=CARTESIAN_POINT ( 'NONE',  ( 2.000000000000011990, -0.1960773996331451885, 0.5999999999999923173 ) ) ;
#54429=ORIENTED_EDGE ( 'NONE', *, *, #170447, .F. ) ;
#54637=CARTESIAN_POINT ( 'NONE',  ( -2.680963302752292332, 0.4788041664876945269, 8.638326563840814180E-32 ) ) ;
#54800=DIRECTION ( 'NONE',  ( 8.638326563840814399E-31, 0.000000000000000000, 1.000000000000000000 ) ) ;
#54908=CARTESIAN_POINT ( 'NONE',  ( 1.324925973730993745, -1.296446089449550421, 1.500000000000000666 ) ) ;
#55163=EDGE_CURVE ( 'NONE', #47720, #120769, #134920, .T. ) ;
#55164=VECTOR ( 'NONE', #138306, 1000.000000000000000 ) ;
#55630=DIRECTION ( 'NONE',  ( -1.000000000000000000, 7.047314121155791443E-15, -8.638326563840826660E-31 ) ) ;
#55794=EDGE_CURVE ( 'NONE', #138769, #148041, #40699, .T. ) ;
#55975=AXIS2_PLACEMENT_3D ( 'NONE', #9350, #89556, #75422 ) ;
#55976=CARTESIAN_POINT ( 'NONE',  ( 1.237941840314000785, -1.374772708486730943, 1.500000000000001332 ) ) ;
#56243=CARTESIAN_POINT ( 'NONE',  ( 1.324887192667550062, 1.296481010641095777, 1.500000000000000888 ) ) ;
#56552=CIRCLE ( 'NONE', #18493, 1.850000000000000089 ) ;
#56717=( LENGTH_UNIT ( ) NAMED_UNIT ( * ) SI_UNIT ( .MILLI., .METRE. ) );
#56843=CIRCLE ( 'NONE', #177933, 0.09999999999999982514 ) ;
#56979=DIRECTION ( 'NONE',  ( 8.638326563840814399E-31, 0.000000000000000000, 1.000000000000000000 ) ) ;
#57611=( GEOMETRIC_REPRESENTATION_CONTEXT ( 3 ) GLOBAL_UNCERTAINTY_ASSIGNED_CONTEXT ( ( #72303 ) ) GLOBAL_UNIT_ASSIGNED_CONTEXT ( ( #139680, #91994, #158054 ) ) REPRESENTATION_CONTEXT ( 'NONE', 'WORKASPACE' ) );
#57781=SURFACE_STYLE_USAGE ( .BOTH. , #185629 ) ;
#57848=CARTESIAN_POINT ( 'NONE',  ( 1.777638883463141806, 0.9165151389911742053, 1.199999999999999734 ) ) ;
#57901=VECTOR ( 'NONE', #56979, 1000.000000000000000 ) ;
#57948=DIRECTION ( 'NONE',  ( -8.638326563840814399E-31, 0.000000000000000000, -1.000000000000000000 ) ) ;
#58450=B_SPLINE_CURVE_WITH_KNOTS ( 'NONE', 3,
 ( #4776, #130887, #98324, #118635, #196881, #114640, #164389, #18915 ),
 .UNSPECIFIED., .F., .F.,
 ( 4, 2, 2, 4 ),
 ( 0.0003136881264510912523, 0.0009048594355810784130, 0.001200445090146071885, 0.001496030744711065140 ),
 .UNSPECIFIED. ) ;
#59166=CARTESIAN_POINT ( 'NONE',  ( 1.607015867998833336, -0.9165151389911481150, 1.199999999999999734 ) ) ;
#59258=CARTESIAN_POINT ( 'NONE',  ( -1.580803134831892276, 0.9624764945123778226, 1.305310695360494710 ) ) ;
#59766=CARTESIAN_POINT ( 'NONE',  ( -2.641766398689996187, -0.3984423641809051175, -0.1533590935930825572 ) ) ;
#59811=CARTESIAN_POINT ( 'NONE',  ( 2.651186565980344856, -0.4067314603539678441, -0.1428011528578489453 ) ) ;
#59820=( GEOMETRIC_REPRESENTATION_CONTEXT ( 3 ) GLOBAL_UNCERTAINTY_ASSIGNED_CONTEXT ( ( #117724 ) ) GLOBAL_UNIT_ASSIGNED_CONTEXT ( ( #20792, #39202, #157239 ) ) REPRESENTATION_CONTEXT ( 'NONE', 'WORKASPACE' ) );
#60025=DIRECTION ( 'NONE',  ( 8.638326563840814399E-31, 0.000000000000000000, 1.000000000000000000 ) ) ;
#60373=CARTESIAN_POINT ( 'NONE',  ( -2.540289672789929121, -0.3621416576072680749, -0.2590487051680252506 ) ) ;
#60453=CARTESIAN_POINT ( 'NONE',  ( -2.680963302752292332, 0.4788041664876945269, -8.638326563840810896E-32 ) ) ;
#60729=CARTESIAN_POINT ( 'NONE',  ( -1.237941840313982578, -1.374772708486751593, 1.500000000000001332 ) ) ;
#60912=AXIS2_PLACEMENT_3D ( 'NONE', #150577, #70342, #21582 ) ;
#61095=CARTESIAN_POINT ( 'NONE',  ( 0.000000000000000000, 0.000000000000000000, -0.5000000000000004441 ) ) ;
#61180=CARTESIAN_POINT ( 'NONE',  ( 1.527869225950146292, 1.291745156262789074, 1.495028600074751468 ) ) ;
#61560=B_SPLINE_CURVE_WITH_KNOTS ( 'NONE', 3,
 ( #76829, #45425, #29158, #95249, #161298, #145082, #211085, #135995 ),
 .UNSPECIFIED., .F., .F.,
 ( 4, 2, 2, 4 ),
 ( 0.0001232303426307903009, 0.0004276537133814902261, 0.0005798653987568402023, 0.0007320770841321901784 ),
 .UNSPECIFIED. ) ;
#61623=CARTESIAN_POINT ( 'NONE',  ( -5.249999999999987566, 0.000000000000000000, 1.599999999999997202 ) ) ;
#61692=DIRECTION ( 'NONE',  ( -1.000000000000000000, 0.000000000000000000, -8.638326563840826660E-31 ) ) ;
#61950=CARTESIAN_POINT ( 'NONE',  ( 2.642331537210453440, -0.3998488639457564719, -0.1525862845480549512 ) ) ;
#62039=AXIS2_PLACEMENT_3D ( 'NONE', #176425, #46427, #125622 ) ;
#62042=EDGE_CURVE ( 'NONE', #122458, #47720, #61560, .T. ) ;
#62251=VERTEX_POINT ( 'NONE', #37413 ) ;
#63009=ORIENTED_EDGE ( 'NONE', *, *, #84492, .F. ) ;
#63023=ORIENTED_EDGE ( 'NONE', *, *, #50862, .F. ) ;
#63031=ORIENTED_EDGE ( 'NONE', *, *, #200985, .T. ) ;
#63060=EDGE_CURVE ( 'NONE', #52075, #116404, #20638, .T. ) ;
#63314=CARTESIAN_POINT ( 'NONE',  ( 1.777638883463141806, 0.9165151389911742053, 1.199999999999999734 ) ) ;
#63815=B_SPLINE_CURVE_WITH_KNOTS ( 'NONE', 3,
 ( #35905, #153937, #185348, #136626, #21757, #34829 ),
 .UNSPECIFIED., .F., .F.,
 ( 4, 2, 4 ),
 ( 0.000000000000000000, 0.0003346294579448544793, 0.0006692589158897089587 ),
 .UNSPECIFIED. ) ;
#64005=STYLED_ITEM ( 'NONE', ( #22040 ), #86932 ) ;
#64469=CARTESIAN_POINT ( 'NONE',  ( -2.621219598810449636, 0.3864874759363081114, -0.1754412237054647494 ) ) ;
#64524=EDGE_CURVE ( 'NONE', #106638, #122127, #174015, .T. ) ;
#64667=CARTESIAN_POINT ( 'NONE',  ( 2.000000000000011990, 2.453103989352373237E-14, 0.5999999999999970912 ) ) ;
#64697=ORIENTED_EDGE ( 'NONE', *, *, #46655, .F. ) ;
#64732=VECTOR ( 'NONE', #206860, 1000.000000000000000 ) ;
#64979=ORIENTED_EDGE ( 'NONE', *, *, #84492, .T. ) ;
#65111=DIRECTION ( 'NONE',  ( 1.000000000000000000, 0.000000000000000000, 8.638326563840826660E-31 ) ) ;
#65152=CARTESIAN_POINT ( 'NONE',  ( 2.651925681381814837, 0.4070128260628380068, -0.1420391113308220876 ) ) ;
#65155=AXIS2_PLACEMENT_3D ( 'NONE', #76147, #190946, #55630 ) ;
#65254=CARTESIAN_POINT ( 'NONE',  ( -2.324999999999998845, 0.000000000000000000, -0.5000000000000004441 ) ) ;
#65415=CARTESIAN_POINT ( 'NONE',  ( 1.596166908135342233, 1.206333752204394871, 1.472837400516055606 ) ) ;
#65591=ORIENTED_EDGE ( 'NONE', *, *, #17510, .F. ) ;
#65654=CARTESIAN_POINT ( 'NONE',  ( -2.580963302752292243, 0.4788041664876945269, 0.000000000000000000 ) ) ;
#65677=EDGE_CURVE ( 'NONE', #116404, #182073, #81879, .T. ) ;
#65746=CARTESIAN_POINT ( 'NONE',  ( -2.609770642201835855, 0.3830433331901538785, 0.000000000000000000 ) ) ;
#66003=ADVANCED_FACE ( 'NONE', ( #198788 ), #209982, .F. ) ;
#66076=PRESENTATION_STYLE_ASSIGNMENT (( #16267 ) ) ;
#66148=ORIENTED_EDGE ( 'NONE', *, *, #179634, .F. ) ;
#66230=DIRECTION ( 'NONE',  ( -1.000000000000000000, 0.000000000000000000, 0.000000000000000000 ) ) ;
#66279=ADVANCED_FACE ( 'NONE', ( #141335, #42749 ), #192149, .F. ) ;
#66571=EDGE_LOOP ( 'NONE', ( #189406, #162792, #38521, #212928 ) ) ;
#68159=B_SPLINE_CURVE_WITH_KNOTS ( 'NONE', 3,
 ( #194201, #175841, #9051, #211506, #210441, #109830 ),
 .UNSPECIFIED., .F., .F.,
 ( 4, 2, 4 ),
 ( 0.001496030744711039119, 0.002086206484339677911, 0.002676382223968317136 ),
 .UNSPECIFIED. ) ;
#68249=ORIENTED_EDGE ( 'NONE', *, *, #108709, .F. ) ;
#68325=ORIENTED_EDGE ( 'NONE', *, *, #39143, .T. ) ;
#68487=DIRECTION ( 'NONE',  ( 8.638326563840814399E-31, 0.000000000000000000, 1.000000000000000000 ) ) ;
#68547=VECTOR ( 'NONE', #207978, 1000.000000000000000 ) ;
#69457=CARTESIAN_POINT ( 'NONE',  ( -1.452583904633382383, -1.374772708486751593, 1.500000000000001332 ) ) ;
#69902=VECTOR ( 'NONE', #11115, 1000.000000000000000 ) ;
#70192=FACE_OUTER_BOUND ( 'NONE', #38936, .T. ) ;
#70342=DIRECTION ( 'NONE',  ( 1.000000000000000000, 1.725633230170963762E-31, 8.638326563840814399E-31 ) ) ;
#70457=ORIENTED_EDGE ( 'NONE', *, *, #200070, .T. ) ;
#70604=SURFACE_SIDE_STYLE ('',( #105294 ) ) ;
#70611=DIRECTION ( 'NONE',  ( -1.000000000000000000, -3.451266460341926649E-31, 0.000000000000000000 ) ) ;
#71079=CARTESIAN_POINT ( 'NONE',  ( -1.452583904633382383, -1.374772708486751593, 1.500000000000001332 ) ) ;
#71186=VERTEX_POINT ( 'NONE', #36656 ) ;
#71393=EDGE_CURVE ( 'NONE', #92178, #25559, #156067, .T. ) ;
#71589=CARTESIAN_POINT ( 'NONE',  ( -1.527869225950100107, -1.291745156262765759, 1.495028600074747027 ) ) ;
#72031=CARTESIAN_POINT ( 'NONE',  ( -2.609770642201835855, 0.3830433331901555993, -0.1872689674646474400 ) ) ;
#72089=DIRECTION ( 'NONE',  ( 1.000000000000000000, 3.451266460341926649E-31, 8.638326563840809144E-31 ) ) ;
#72303=UNCERTAINTY_MEASURE_WITH_UNIT (LENGTH_MEASURE( 1.000000000000000082E-05 ), #139680, 'distance_accuracy_value', 'NONE');
#72324=ADVANCED_FACE ( 'NONE', ( #30025 ), #125473, .F. ) ;
#72460=CARTESIAN_POINT ( 'NONE',  ( 2.325000000000005063, -1.380506584136773856E-31, -3.455330625536332679E-31 ) ) ;
#72758=FILL_AREA_STYLE ('',( #121605 ) ) ;
#72946=CARTESIAN_POINT ( 'NONE',  ( 1.876320386020374986, 0.7120587666045359310, 0.8722162550184342500 ) ) ;
#73157=CARTESIAN_POINT ( 'NONE',  ( -2.679285714285713826, 0.4970443252110372523, -0.5000000000000004441 ) ) ;
#73298=B_SPLINE_CURVE_WITH_KNOTS ( 'NONE', 3,
 ( #13574, #64469, #193398, #146813, #180351, #128495, #213878, #99108, #95928, #78575, #210708, #161984, #197649, #14628, #179299, #195540 ),
 .UNSPECIFIED., .F., .F.,
 ( 4, 3, 3, 3, 3, 4 ),
 ( 6.327738642270367575E-19, 5.045320844140702436E-05, 9.514731479413830913E-05, 0.0001285019506255545335, 0.0001554096905450522809, 0.0001555421464865875856 ),
 .UNSPECIFIED. ) ;
#73400=CARTESIAN_POINT ( 'NONE',  ( -2.679285714285713826, 0.4970443252110354759, 0.000000000000000000 ) ) ;
#73420=EDGE_CURVE ( 'NONE', #133104, #171149, #44708, .T. ) ;
#73694=CARTESIAN_POINT ( 'NONE',  ( 2.679285714285720044, 0.4970443252110459120, -0.09999999999999592548 ) ) ;
#73704=AXIS2_PLACEMENT_3D ( 'NONE', #78379, #94662, #113090 ) ;
#73891=CARTESIAN_POINT ( 'NONE',  ( -2.678032581596935024, -0.4534618882029449183, -0.1088563323523765447 ) ) ;
#74036=CARTESIAN_POINT ( 'NONE',  ( 1.992392395334954491, 0.1979219324388767909, 0.6149939648490070354 ) ) ;
#74158=DIRECTION ( 'NONE',  ( -1.000000000000000000, -3.451266460341926649E-31, -8.638326563840809144E-31 ) ) ;
#74654=SURFACE_STYLE_USAGE ( .BOTH. , #89858 ) ;
#75121=ORIENTED_EDGE ( 'NONE', *, *, #189935, .F. ) ;
#75197=VECTOR ( 'NONE', #99739, 1000.000000000000000 ) ;
#75422=DIRECTION ( 'NONE',  ( 1.000000000000000000, 3.451266460341926649E-31, 8.638326563840810896E-31 ) ) ;
#75895=EDGE_LOOP ( 'NONE', ( #121568, #43530, #50522, #210129 ) ) ;
#76020=CARTESIAN_POINT ( 'NONE',  ( -2.630984769852970917, -0.3922140236936322299, -0.1649412225328064641 ) ) ;
#76092=CYLINDRICAL_SURFACE ( 'NONE', #193271, 2.725000000000000089 ) ;
#76147=CARTESIAN_POINT ( 'NONE',  ( 2.580963302752299349, -0.4788041664876945269, 0.000000000000000000 ) ) ;
#76472=DIRECTION ( 'NONE',  ( 1.000000000000000000, 3.451266460341926649E-31, 8.638326563840809144E-31 ) ) ;
#76829=CARTESIAN_POINT ( 'NONE',  ( -2.609770642201835855, 0.3830433331901555993, -0.1872689674646474400 ) ) ;
#76864=ORIENTED_EDGE ( 'NONE', *, *, #189585, .T. ) ;
#76943=CARTESIAN_POINT ( 'NONE',  ( 1.607015867998833336, -0.9165151389911481150, 1.199999999999999734 ) ) ;
#77237=CARTESIAN_POINT ( 'NONE',  ( -5.249999999999987566, -1.374772708486751593, 1.000000000000000888 ) ) ;
#77337=LINE ( 'NONE', #106693, #182976 ) ;
#77550=CARTESIAN_POINT ( 'NONE',  ( -2.679285714285713826, -0.4970443252110337551, -0.5000000000000004441 ) ) ;
#77988=LINE ( 'NONE', #190657, #68547 ) ;
#78379=CARTESIAN_POINT ( 'NONE',  ( 0.000000000000000000, 0.000000000000000000, -0.5000000000000004441 ) ) ;
#78575=CARTESIAN_POINT ( 'NONE',  ( -2.677589438261867016, 0.4530478092824221648, -0.1093532045961659316 ) ) ;
#78591=CARTESIAN_POINT ( 'NONE',  ( 1.713667314260276076, -1.036161614632699957, 1.380621972511351547 ) ) ;
#78619=AXIS2_PLACEMENT_3D ( 'NONE', #84690, #203744, #167017 ) ;
#78748=ORIENTED_EDGE ( 'NONE', *, *, #169097, .T. ) ;
#78752=CARTESIAN_POINT ( 'NONE',  ( -2.474351396550309445, -0.3224749582910480528, -0.3303680917369637426 ) ) ;
#79215=CARTESIAN_POINT ( 'NONE',  ( -2.651925681381809952, -0.4070128260628267935, -0.1420391113308281661 ) ) ;
#79631=ADVANCED_FACE ( 'NONE', ( #85495 ), #86567, .T. ) ;
#79765=UNCERTAINTY_MEASURE_WITH_UNIT (LENGTH_MEASURE( 1.000000000000000082E-05 ), #187316, 'distance_accuracy_value', 'NONE');
#80265=ORIENTED_EDGE ( 'NONE', *, *, #96386, .F. ) ;
#80317=DIRECTION ( 'NONE',  ( 8.638326563840814399E-31, 0.000000000000000000, 1.000000000000000000 ) ) ;
#80468=ORIENTED_EDGE ( 'NONE', *, *, #94915, .T. ) ;
#80701=VECTOR ( 'NONE', #170354, 1000.000000000000000 ) ;
#81037=B_SPLINE_CURVE_WITH_KNOTS ( 'NONE', 3,
 ( #10899, #107422, #90058, #173447, #157185, #60729 ),
 .UNSPECIFIED., .F., .F.,
 ( 4, 2, 4 ),
 ( 0.000000000000000000, 0.0003473417695167272832, 0.0006946835390334545664 ),
 .UNSPECIFIED. ) ;
#81112=CIRCLE ( 'NONE', #18787, 2.324999999999998845 ) ;
#81617=FACE_OUTER_BOUND ( 'NONE', #90107, .T. ) ;
#81685=ORIENTED_EDGE ( 'NONE', *, *, #29276, .F. ) ;
#81879=B_SPLINE_CURVE_WITH_KNOTS ( 'NONE', 3,
 ( #172190, #108315, #155936, #139705, #207862, #92022 ),
 .UNSPECIFIED., .F., .F.,
 ( 4, 2, 4 ),
 ( 0.001496030744711065140, 0.002086206484339691788, 0.002676382223968318437 ),
 .UNSPECIFIED. ) ;
#81898=UNCERTAINTY_MEASURE_WITH_UNIT (LENGTH_MEASURE( 1.000000000000000082E-05 ), #108750, 'distance_accuracy_value', 'NONE');
#81941=ORIENTED_EDGE ( 'NONE', *, *, #46655, .T. ) ;
#82369=VECTOR ( 'NONE', #76472, 1000.000000000000000 ) ;
#82524=CARTESIAN_POINT ( 'NONE',  ( 2.325000000000005063, 0.000000000000000000, -0.5000000000000004441 ) ) ;
#83258=ORIENTED_EDGE ( 'NONE', *, *, #154305, .F. ) ;
#83708=ORIENTED_EDGE ( 'NONE', *, *, #199736, .F. ) ;
#83925=MECHANICAL_DESIGN_GEOMETRIC_PRESENTATION_REPRESENTATION('',(#35529),#59820);
#84455=CARTESIAN_POINT ( 'NONE',  ( 2.679285714285720044, 0.4970443252110459120, 0.000000000000000000 ) ) ;
#84492=EDGE_CURVE ( 'NONE', #89282, #120769, #20439, .T. ) ;
#84690=CARTESIAN_POINT ( 'NONE',  ( 2.580963302752299349, 0.4788041664877049075, 0.000000000000000000 ) ) ;
#84835=CARTESIAN_POINT ( 'NONE',  ( -1.607015867998808023, -0.9165151389911689872, 1.199999999999999734 ) ) ;
#84957=B_SPLINE_CURVE_WITH_KNOTS ( 'NONE', 3,
 ( #55976, #54908, #188092, #138303, #206479, #59166 ),
 .UNSPECIFIED., .F., .F.,
 ( 4, 2, 4 ),
 ( 2.491306920542262691E-18, 0.0003472644472073823057, 0.0006945288944147621178 ),
 .UNSPECIFIED. ) ;
#85224=LINE ( 'NONE', #65746, #203221 ) ;
#85328=VERTEX_POINT ( 'NONE', #153043 ) ;
#85495=FACE_OUTER_BOUND ( 'NONE', #208163, .T. ) ;
#85685=CARTESIAN_POINT ( 'NONE',  ( 2.680963302752255029, 0.4759847170802535832, -0.1021121987831403316 ) ) ;
#86386=CARTESIAN_POINT ( 'NONE',  ( 1.850000000000000089, 4.013456704145457099E-20, 0.5999999999999969802 ) ) ;
#86567=PLANE ( 'NONE',  #132350 ) ;
#86887=DIRECTION ( 'NONE',  ( 0.000000000000000000, 0.000000000000000000, -1.000000000000000000 ) ) ;
#86921=ORIENTED_EDGE ( 'NONE', *, *, #111248, .F. ) ;
#86932=MANIFOLD_SOLID_BREP ( 'Fillet3', #101943 ) ;
#87041=EDGE_CURVE ( 'NONE', #3254, #174147, #203806, .T. ) ;
#87171=CARTESIAN_POINT ( 'NONE',  ( -2.679285714285713826, 0.4970443252110354759, -0.09999999999999592548 ) ) ;
#87253=CIRCLE ( 'NONE', #149559, 2.725000000000000089 ) ;
#87281=ORIENTED_EDGE ( 'NONE', *, *, #100563, .T. ) ;
#87337=EDGE_CURVE ( 'NONE', #4447, #167565, #8504, .T. ) ;
#88006=CARTESIAN_POINT ( 'NONE',  ( -2.679885790744698681, -0.4618020869171932108, -0.1056289066552756756 ) ) ;
#88041=ORIENTED_EDGE ( 'NONE', *, *, #113537, .T. ) ;
#88165=( NAMED_UNIT ( * ) PLANE_ANGLE_UNIT ( ) SI_UNIT ( $, .RADIAN. ) );
#88219=CARTESIAN_POINT ( 'NONE',  ( 0.000000000000000000, 0.000000000000000000, 0.000000000000000000 ) ) ;
#88355=ORIENTED_EDGE ( 'NONE', *, *, #63060, .T. ) ;
#88391=CIRCLE ( 'NONE', #209417, 2.000000000000000000 ) ;
#88507=ORIENTED_EDGE ( 'NONE', *, *, #71393, .T. ) ;
#88692=ORIENTED_EDGE ( 'NONE', *, *, #40961, .F. ) ;
#88745=LINE ( 'NONE', #72460, #33078 ) ;
#88893=VERTEX_POINT ( 'NONE', #137497 ) ;
#89020=B_SPLINE_CURVE_WITH_KNOTS ( 'NONE', 3,
 ( #195835, #130899, #214163, #131938, #46396, #98335, #14920, #164401 ),
 .UNSPECIFIED., .F., .F.,
 ( 4, 2, 2, 4 ),
 ( 0.0007320770841321888774, 0.0008843033762534638440, 0.001036529668374738811, 0.001340982252617288093 ),
 .UNSPECIFIED. ) ;
#89086=EDGE_CURVE ( 'NONE', #146443, #140937, #88745, .T. ) ;
#89091=CARTESIAN_POINT ( 'NONE',  ( -2.671705178897693322, -0.4353224022266648507, -0.1180795802420711998 ) ) ;
#89282=VERTEX_POINT ( 'NONE', #207794 ) ;
#89492=B_SPLINE_CURVE_WITH_KNOTS ( 'NONE', 3,
 ( #32716, #119363, #148610, #18586, #98798, #16444, #19654, #82524 ),
 .UNSPECIFIED., .F., .F.,
 ( 4, 2, 2, 4 ),
 ( 0.0001232303426307903009, 0.0004276537133814895756, 0.0005798653987568392265, 0.0007320770841321888774 ),
 .UNSPECIFIED. ) ;
#89556=DIRECTION ( 'NONE',  ( 8.638326563840814399E-31, 0.000000000000000000, 1.000000000000000000 ) ) ;
#89564=CARTESIAN_POINT ( 'NONE',  ( 1.850000000000000089, 6.384842951632563950E-31, -5.732590180780448463 ) ) ;
#89822=DIRECTION ( 'NONE',  ( -8.638326563840814399E-31, 0.000000000000000000, -1.000000000000000000 ) ) ;
#89858=SURFACE_SIDE_STYLE ('',( #109358 ) ) ;
#89921=DIRECTION ( 'NONE',  ( 8.638326563840814399E-31, -0.000000000000000000, 1.000000000000000000 ) ) ;
#90058=CARTESIAN_POINT ( 'NONE',  ( -1.532927541463133592, -1.041115454748546609, 1.384885517283066525 ) ) ;
#90107=EDGE_LOOP ( 'NONE', ( #190086, #6420 ) ) ;
#90466=CYLINDRICAL_SURFACE ( 'NONE', #147362, 0.09999999999999982514 ) ;
#90483=ADVANCED_FACE ( 'NONE', ( #174026 ), #123212, .T. ) ;
#90556=APPLICATION_CONTEXT ( 'automotive_design' ) ;
#90639=DIRECTION ( 'NONE',  ( -8.638326563840814399E-31, 0.000000000000000000, -1.000000000000000000 ) ) ;
#90682=CARTESIAN_POINT ( 'NONE',  ( -5.249999999999987566, 0.9165151389911689872, 1.199999999999999734 ) ) ;
#90754=EDGE_CURVE ( 'NONE', #187511, #134057, #8956, .T. ) ;
#91272=CARTESIAN_POINT ( 'NONE',  ( -5.249999999999987566, 0.000000000000000000, 0.5999999999999969802 ) ) ;
#91302=CARTESIAN_POINT ( 'NONE',  ( 0.000000000000000000, 0.000000000000000000, -0.5000000000000004441 ) ) ;
#91471=STYLED_ITEM ( 'NONE', ( #66076 ), #7315 ) ;
#91703=ORIENTED_EDGE ( 'NONE', *, *, #189585, .F. ) ;
#91994=( NAMED_UNIT ( * ) PLANE_ANGLE_UNIT ( ) SI_UNIT ( $, .RADIAN. ) );
#92013=ORIENTED_EDGE ( 'NONE', *, *, #113537, .F. ) ;
#92022=CARTESIAN_POINT ( 'NONE',  ( -1.607015867998808023, -0.9165151389911689872, 1.199999999999999734 ) ) ;
#92046=DIRECTION ( 'NONE',  ( -8.638326563840814399E-31, 0.000000000000000000, -1.000000000000000000 ) ) ;
#92126=CARTESIAN_POINT ( 'NONE',  ( -2.679285714285713826, 0.4970443252110354759, -0.09999999999999592548 ) ) ;
#92178=VERTEX_POINT ( 'NONE', #71079 ) ;
#92772=DIRECTION ( 'NONE',  ( -1.000000000000000000, 0.000000000000000000, 0.000000000000000000 ) ) ;
#93620=DIRECTION ( 'NONE',  ( 1.000000000000000000, 3.451266460341926649E-31, 0.000000000000000000 ) ) ;
#93873=AXIS2_PLACEMENT_3D ( 'NONE', #33031, #199773, #182460 ) ;
#94128=PRESENTATION_STYLE_ASSIGNMENT (( #74654 ) ) ;
#94662=DIRECTION ( 'NONE',  ( -8.638326563840814399E-31, 0.000000000000000000, -1.000000000000000000 ) ) ;
#94759=AXIS2_PLACEMENT_3D ( 'NONE', #128302, #12299, #31783 ) ;
#94915=EDGE_CURVE ( 'NONE', #182073, #106638, #81037, .T. ) ;
#95216=CARTESIAN_POINT ( 'NONE',  ( 0.000000000000000000, 0.000000000000000000, 0.000000000000000000 ) ) ;
#95249=CARTESIAN_POINT ( 'NONE',  ( -2.393657244693855990, 0.2279079664470276545, -0.4206872822309645210 ) ) ;
#95928=CARTESIAN_POINT ( 'NONE',  ( -2.674941732306335140, 0.4431148209949185568, -0.1136209127918899470 ) ) ;
#96386=EDGE_CURVE ( 'NONE', #101960, #146443, #50534, .T. ) ;
#96528=CARTESIAN_POINT ( 'NONE',  ( -1.777638883463106279, 0.9165151389911794233, 1.199999999999999734 ) ) ;
#96628=ORIENTED_EDGE ( 'NONE', *, *, #39143, .F. ) ;
#96882=COLOUR_RGB ( '', 0.08235294, 0.09019608, 0.10196078) ;
#96910=CARTESIAN_POINT ( 'NONE',  ( 1.491410138560286924, 1.333748936243118077, 1.500000000000000888 ) ) ;
#97359=UNCERTAINTY_MEASURE_WITH_UNIT (LENGTH_MEASURE( 1.000000000000000082E-05 ), #56717, 'distance_accuracy_value', 'NONE');
#97585=CARTESIAN_POINT ( 'NONE',  ( -1.999999999999988232, 0.1960773996332039470, 0.6000000000000017542 ) ) ;
#97862=EDGE_CURVE ( 'NONE', #171541, #10112, #50676, .T. ) ;
#98209=DIRECTION ( 'NONE',  ( -1.000000000000000000, 0.000000000000000000, -8.638326563840826660E-31 ) ) ;
#98289=CIRCLE ( 'NONE', #105113, 0.4000000000000010214 ) ;
#98324=CARTESIAN_POINT ( 'NONE',  ( -1.715338164143663136, 0.7127732114542476571, 0.8729459113246227364 ) ) ;
#98335=CARTESIAN_POINT ( 'NONE',  ( 2.474351396550318771, 0.3224749582910498846, -0.3303680917369555270 ) ) ;
#98622=SURFACE_STYLE_FILL_AREA ( #32546 ) ;
#98798=CARTESIAN_POINT ( 'NONE',  ( 2.370002892456526844, -0.1903694832692610361, -0.4477549104883266629 ) ) ;
#98801=ORIENTED_EDGE ( 'NONE', *, *, #55794, .T. ) ;
#99108=CARTESIAN_POINT ( 'NONE',  ( -2.670845766169893665, 0.4339950243563579502, -0.1191324417346312919 ) ) ;
#99679=FILL_AREA_STYLE_COLOUR ( '', #212504 ) ;
#99739=DIRECTION ( 'NONE',  ( -1.000000000000000000, -3.451266460341926649E-31, -8.638326563840809144E-31 ) ) ;
#99753=SHAPE_REPRESENTATION ( 'cover for positive', ( #200407 ), #155604 ) ;
#99812=CARTESIAN_POINT ( 'NONE',  ( 2.660307654469997285, 0.4179397774614675987, -0.1320628536826753963 ) ) ;
#99898=CARTESIAN_POINT ( 'NONE',  ( 0.000000000000000000, 0.000000000000000000, 0.000000000000000000 ) ) ;
#100412=CARTESIAN_POINT ( 'NONE',  ( 1.841702881098854272, -0.1987311101661408952, 0.6151380925063543170 ) ) ;
#100563=EDGE_CURVE ( 'NONE', #89282, #110706, #116604, .T. ) ;
#100906=CYLINDRICAL_SURFACE ( 'NONE', #162210, 1.000000000000000222 ) ;
#100911=CARTESIAN_POINT ( 'NONE',  ( -1.876320386020336795, -0.7120587666045246067, 0.8722162550184210383 ) ) ;
#101294=AXIS2_PLACEMENT_3D ( 'NONE', #61623, #130703, #196694 ) ;
#101725=ORIENTED_EDGE ( 'NONE', *, *, #109311, .F. ) ;
#101943=CLOSED_SHELL ( 'NONE', ( #40744, #157979, #72324, #124284, #192369, #171348, #44684, #109706, #102444, #178835, #90483, #113804, #42102, #79631, #66279, #104742, #146474, #119184, #140120, #182391, #164270, #199667, #172838, #105427, #154242, #66003, #197875, #177196, #16748, #7315 ) ) ;
#101960=VERTEX_POINT ( 'NONE', #213499 ) ;
#102444=ADVANCED_FACE ( 'NONE', ( #134448 ), #36897, .T. ) ;
#102456=ORIENTED_EDGE ( 'NONE', *, *, #170447, .T. ) ;
#102584=EDGE_CURVE ( 'NONE', #120769, #187511, #9731, .T. ) ;
#103011=CARTESIAN_POINT ( 'NONE',  ( 2.609770642201841184, 0.3830433331901660354, -0.1872689674646474400 ) ) ;
#103039=FACE_OUTER_BOUND ( 'NONE', #122850, .T. ) ;
#103103=ORIENTED_EDGE ( 'NONE', *, *, #112585, .F. ) ;
#103332=CARTESIAN_POINT ( 'NONE',  ( 1.777638883463141806, 0.9165151389911742053, 1.199999999999999734 ) ) ;
#103536=VERTEX_POINT ( 'NONE', #43089 ) ;
#103592=CARTESIAN_POINT ( 'NONE',  ( 2.725000000000005862, 0.000000000000000000, 0.000000000000000000 ) ) ;
#103636=ORIENTED_EDGE ( 'NONE', *, *, #207633, .T. ) ;
#103815=( GEOMETRIC_REPRESENTATION_CONTEXT ( 3 ) GLOBAL_UNCERTAINTY_ASSIGNED_CONTEXT ( ( #137887 ) ) GLOBAL_UNIT_ASSIGNED_CONTEXT ( ( #198809, #138117, #22177 ) ) REPRESENTATION_CONTEXT ( 'NONE', 'WORKASPACE' ) );
#104406=( NAMED_UNIT ( * ) PLANE_ANGLE_UNIT ( ) SI_UNIT ( $, .RADIAN. ) );
#104681=ORIENTED_EDGE ( 'NONE', *, *, #201896, .F. ) ;
#104742=ADVANCED_FACE ( 'NONE', ( #70192 ), #182535, .T. ) ;
#105113=AXIS2_PLACEMENT_3D ( 'NONE', #103592, #151281, #169649 ) ;
#105216=EDGE_LOOP ( 'NONE', ( #167295, #78748, #87281, #168856 ) ) ;
#105242=VERTEX_POINT ( 'NONE', #84455 ) ;
#105294=SURFACE_STYLE_FILL_AREA ( #72758 ) ;
#105427=ADVANCED_FACE ( 'NONE', ( #8529 ), #206728, .F. ) ;
#105904=CARTESIAN_POINT ( 'NONE',  ( 2.725000000000005862, 0.000000000000000000, 0.000000000000000000 ) ) ;
#106138=CYLINDRICAL_SURFACE ( 'NONE', #19556, 0.5000000000000000000 ) ;
#106174=AXIS2_PLACEMENT_3D ( 'NONE', #77237, #162781, #29573 ) ;
#106354=VERTEX_POINT ( 'NONE', #11595 ) ;
#106638=VERTEX_POINT ( 'NONE', #641 ) ;
#106693=CARTESIAN_POINT ( 'NONE',  ( -1.999999999999988010, 2.428612866367529932E-14, 1.500000000000001332 ) ) ;
#106901=EDGE_LOOP ( 'NONE', ( #143646, #80265, #189458, #30687 ) ) ;
#107280=DIRECTION ( 'NONE',  ( -1.000000000000000000, -7.047314121155791443E-15, -8.638326563840826660E-31 ) ) ;
#107422=CARTESIAN_POINT ( 'NONE',  ( -1.580854408705412606, -0.9623865910009720137, 1.305104700536227735 ) ) ;
#107614=VERTEX_POINT ( 'NONE', #73694 ) ;
#107661=PRODUCT ( 'cover for positive', 'cover for positive', '', ( #197768 ) ) ;
#107702=ORIENTED_EDGE ( 'NONE', *, *, #51590, .T. ) ;
#107777=DIRECTION ( 'NONE',  ( -8.638326563840814399E-31, 0.000000000000000000, -1.000000000000000000 ) ) ;
#108007=DIRECTION ( 'NONE',  ( 8.638326563840814399E-31, -0.000000000000000000, 1.000000000000000000 ) ) ;
#108200=ORIENTED_EDGE ( 'NONE', *, *, #207059, .T. ) ;
#108315=CARTESIAN_POINT ( 'NONE',  ( -1.850000000000000089, -0.1967728318288185785, 0.5999999999999968692 ) ) ;
#108709=EDGE_CURVE ( 'NONE', #101960, #62251, #37740, .T. ) ;
#108750=( LENGTH_UNIT ( ) NAMED_UNIT ( * ) SI_UNIT ( .MILLI., .METRE. ) );
#109125=ORIENTED_EDGE ( 'NONE', *, *, #200070, .F. ) ;
#109311=EDGE_CURVE ( 'NONE', #107614, #138769, #181359, .T. ) ;
#109358=SURFACE_STYLE_FILL_AREA ( #43241 ) ;
#109706=ADVANCED_FACE ( 'NONE', ( #187988 ), #123107, .T. ) ;
#109830=CARTESIAN_POINT ( 'NONE',  ( 1.607015867998825343, 0.9165151389911689872, 1.199999999999999734 ) ) ;
#110178=AXIS2_PLACEMENT_3D ( 'NONE', #184266, #21745, #66230 ) ;
#110706=VERTEX_POINT ( 'NONE', #17487 ) ;
#111170=CARTESIAN_POINT ( 'NONE',  ( 1.777638883463123598, -0.9165151389911446733, 1.199999999999999734 ) ) ;
#111248=EDGE_CURVE ( 'NONE', #107614, #152613, #138904, .T. ) ;
#111709=VERTEX_POINT ( 'NONE', #126695 ) ;
#111729=ORIENTED_EDGE ( 'NONE', *, *, #117853, .F. ) ;
#111839=CARTESIAN_POINT ( 'NONE',  ( 2.609770642201842072, -0.3830433331901555993, -0.1872689674646474400 ) ) ;
#111848=AXIS2_PLACEMENT_3D ( 'NONE', #61095, #60025, #93620 ) ;
#112585=EDGE_CURVE ( 'NONE', #4447, #191630, #7974, .T. ) ;
#112901=CARTESIAN_POINT ( 'NONE',  ( 2.670845766169899438, -0.4339950243563576726, -0.1191324417346315279 ) ) ;
#112957=DIRECTION ( 'NONE',  ( 1.000000000000000000, 3.451266460341926649E-31, 8.638326563840809144E-31 ) ) ;
#112983=CARTESIAN_POINT ( 'NONE',  ( -1.965118028437710995, -0.3835514080770054401, 0.6713998180129590043 ) ) ;
#113090=DIRECTION ( 'NONE',  ( -1.000000000000000000, -3.451266460341926649E-31, 0.000000000000000000 ) ) ;
#113127=PLANE ( 'NONE',  #145834 ) ;
#113537=EDGE_CURVE ( 'NONE', #140937, #47720, #167100, .T. ) ;
#113618=LINE ( 'NONE', #193723, #155400 ) ;
#113788=ORIENTED_EDGE ( 'NONE', *, *, #9722, .F. ) ;
#113804=ADVANCED_FACE ( 'NONE', ( #49096 ), #160705, .T. ) ;
#113972=CARTESIAN_POINT ( 'NONE',  ( 2.680411860343932862, -0.4909739067630093379, -0.09999999999832692721 ) ) ;
#114640=CARTESIAN_POINT ( 'NONE',  ( -1.841702881098853162, 0.1987311101661545787, 0.6151380925063570926 ) ) ;
#114650=CARTESIAN_POINT ( 'NONE',  ( 1.214306433183764966E-14, 2.428612866367529932E-14, 1.500000000000001332 ) ) ;
#115143=DIRECTION ( 'NONE',  ( -1.000000000000000000, -3.451266460341926211E-31, -8.638326563840810896E-31 ) ) ;
#115146=EDGE_LOOP ( 'NONE', ( #210701, #81941, #36048, #101725, #168668, #38657, #75121, #189308 ) ) ;
#115562=DIRECTION ( 'NONE',  ( 8.638326563840814399E-31, -0.000000000000000000, 1.000000000000000000 ) ) ;
#115654=CARTESIAN_POINT ( 'NONE',  ( 1.850000000000000089, 4.013456704145457099E-20, 0.5999999999999969802 ) ) ;
#115751=ORIENTED_EDGE ( 'NONE', *, *, #62042, .T. ) ;
#115848=AXIS2_PLACEMENT_3D ( 'NONE', #208294, #177961, #175834 ) ;
#115927=DIRECTION ( 'NONE',  ( -1.000000000000000000, -3.451266460341926649E-31, -8.638326563840809144E-31 ) ) ;
#115973=LINE ( 'NONE', #49846, #140060 ) ;
#116001=CARTESIAN_POINT ( 'NONE',  ( -1.876272499184424847, 0.7121508056591905333, 0.8723429728170274400 ) ) ;
#116095=ORIENTED_EDGE ( 'NONE', *, *, #188915, .F. ) ;
#116212=ORIENTED_EDGE ( 'NONE', *, *, #189930, .T. ) ;
#116404=VERTEX_POINT ( 'NONE', #177546 ) ;
#116482=ORIENTED_EDGE ( 'NONE', *, *, #5366, .T. ) ;
#116604=CIRCLE ( 'NONE', #40495, 2.725000000000000089 ) ;
#116747=AXIS2_PLACEMENT_3D ( 'NONE', #39046, #5437, #188486 ) ;
#117233=CARTESIAN_POINT ( 'NONE',  ( -1.817809523595264043, -0.8386016503486174445, 1.021477770318699241 ) ) ;
#117252=CARTESIAN_POINT ( 'NONE',  ( 1.777638883463123598, -0.9165151389911446733, 1.199999999999999734 ) ) ;
#117712=EDGE_CURVE ( 'NONE', #47720, #140937, #81112, .T. ) ;
#117724=UNCERTAINTY_MEASURE_WITH_UNIT (LENGTH_MEASURE( 1.000000000000000082E-05 ), #20792, 'distance_accuracy_value', 'NONE');
#117853=EDGE_CURVE ( 'NONE', #111709, #171149, #177926, .T. ) ;
#118299=ORIENTED_EDGE ( 'NONE', *, *, #169097, .F. ) ;
#118483=DIRECTION ( 'NONE',  ( -1.000000000000000000, 0.000000000000000000, -8.638326563840826660E-31 ) ) ;
#118635=CARTESIAN_POINT ( 'NONE',  ( -1.790313668900411992, 0.4735605917218872474, 0.7140520948302793158 ) ) ;
#118767=EDGE_CURVE ( 'NONE', #52075, #103536, #169141, .T. ) ;
#118860=CARTESIAN_POINT ( 'NONE',  ( 1.812013678032661668, -0.3846686717400226163, 0.6718421233638880441 ) ) ;
#119184=ADVANCED_FACE ( 'NONE', ( #204623 ), #122433, .F. ) ;
#119267=ORIENTED_EDGE ( 'NONE', *, *, #90754, .T. ) ;
#119363=CARTESIAN_POINT ( 'NONE',  ( 2.540684401258877401, -0.3622604021566167010, -0.2586409171621159020 ) ) ;
#119412=CARTESIAN_POINT ( 'NONE',  ( 2.680963302754415079, 0.4788041664859938318, -0.1016165050511480955 ) ) ;
#119646=SURFACE_STYLE_FILL_AREA ( #172612 ) ;
#119854=ORIENTED_EDGE ( 'NONE', *, *, #207633, .F. ) ;
#119977=AXIS2_PLACEMENT_3D ( 'NONE', #25951, #89921, #107280 ) ;
#120443=CARTESIAN_POINT ( 'NONE',  ( -1.754679937794462408, -0.9610454613041046201, 1.302031786359981957 ) ) ;
#120535=VECTOR ( 'NONE', #12704, 1000.000000000000000 ) ;
#120743=SURFACE_STYLE_FILL_AREA ( #41569 ) ;
#120769=VERTEX_POINT ( 'NONE', #21887 ) ;
#120997=CARTESIAN_POINT ( 'NONE',  ( 2.680963302752298993, 0.4788041664877049075, 8.638326563840810896E-32 ) ) ;
#121062=LINE ( 'NONE', #89564, #55164 ) ;
#121568=ORIENTED_EDGE ( 'NONE', *, *, #126729, .F. ) ;
#121605=FILL_AREA_STYLE_COLOUR ( '', #180878 ) ;
#122127=VERTEX_POINT ( 'NONE', #17311 ) ;
#122202=CYLINDRICAL_SURFACE ( 'NONE', #213166, 0.4000000000000010214 ) ;
#122229=CARTESIAN_POINT ( 'NONE',  ( -1.324925973730976203, 1.296446089449585948, 1.500000000000001998 ) ) ;
#122417=ADVANCED_BREP_SHAPE_REPRESENTATION ( '', ( #86932, #200407 ), #155604 ) ;
#122433=CYLINDRICAL_SURFACE ( 'NONE', #46659, 0.4000000000000010214 ) ;
#122458=VERTEX_POINT ( 'NONE', #72031 ) ;
#122644=ORIENTED_EDGE ( 'NONE', *, *, #187034, .T. ) ;
#122786=MECHANICAL_DESIGN_GEOMETRIC_PRESENTATION_REPRESENTATION('',(#91471),#25736);
#122797=ORIENTED_EDGE ( 'NONE', *, *, #127726, .T. ) ;
#122850=EDGE_LOOP ( 'NONE', ( #172818, #17030, #137030, #208122, #172646, #207245, #32606, #139778 ) ) ;
#123107=PLANE ( 'NONE',  #42504 ) ;
#123154=CARTESIAN_POINT ( 'NONE',  ( -1.850000000000000089, 2.265596578422597184E-16, 1.540743955509788682E-30 ) ) ;
#123212=CYLINDRICAL_SURFACE ( 'NONE', #181482, 2.000000000000000000 ) ;
#123304=AXIS2_PLACEMENT_3D ( 'NONE', #99898, #168097, #115143 ) ;
#123548=CARTESIAN_POINT ( 'NONE',  ( -2.725000000000000089, 0.000000000000000000, 0.000000000000000000 ) ) ;
#123643=CARTESIAN_POINT ( 'NONE',  ( 2.680963302754415079, 0.4788041664859938318, -0.1016165050511480955 ) ) ;
#123942=CARTESIAN_POINT ( 'NONE',  ( 2.000000000000011990, 2.453103989352373237E-14, 0.5999999999999970912 ) ) ;
#124029=EDGE_CURVE ( 'NONE', #88893, #3254, #166278, .T. ) ;
#124213=CARTESIAN_POINT ( 'NONE',  ( -2.000000000000000000, 2.428612866367544447E-14, 1.733336949948522427E-30 ) ) ;
#124284=ADVANCED_FACE ( 'NONE', ( #35056 ), #52395, .T. ) ;
#124437=CARTESIAN_POINT ( 'NONE',  ( -5.249999999999987566, -0.9165151389911689872, 1.199999999999999734 ) ) ;
#124628=ORIENTED_EDGE ( 'NONE', *, *, #194299, .F. ) ;
#125381=ORIENTED_EDGE ( 'NONE', *, *, #27912, .F. ) ;
#125473=CYLINDRICAL_SURFACE ( 'NONE', #7294, 1.850000000000000089 ) ;
#125622=DIRECTION ( 'NONE',  ( 0.000000000000000000, 0.000000000000000000, -1.000000000000000000 ) ) ;
#125966=CARTESIAN_POINT ( 'NONE',  ( 2.674941732306341358, -0.4431148209949172800, -0.1136209127918897804 ) ) ;
#126110=ORIENTED_EDGE ( 'NONE', *, *, #187034, .F. ) ;
#126180=ORIENTED_EDGE ( 'NONE', *, *, #179393, .F. ) ;
#126275=VERTEX_POINT ( 'NONE', #76943 ) ;
#126382=CARTESIAN_POINT ( 'NONE',  ( -5.249999999999987566, 0.000000000000000000, 1.599999999999997202 ) ) ;
#126531=ORIENTED_EDGE ( 'NONE', *, *, #182196, .F. ) ;
#126536=CARTESIAN_POINT ( 'NONE',  ( -2.324999999999998845, 0.000000000000000000, -0.5000000000000004441 ) ) ;
#126661=ORIENTED_EDGE ( 'NONE', *, *, #191584, .T. ) ;
#126695=CARTESIAN_POINT ( 'NONE',  ( 1.237941840314000785, 1.374772708486753370, 1.500000000000001332 ) ) ;
#126729=EDGE_CURVE ( 'NONE', #171149, #71186, #147868, .T. ) ;
#126806=ORIENTED_EDGE ( 'NONE', *, *, #100563, .F. ) ;
#126937=MECHANICAL_DESIGN_GEOMETRIC_PRESENTATION_REPRESENTATION('',(#147580),#12718);
#127430=B_SPLINE_CURVE_WITH_KNOTS ( 'NONE', 3,
 ( #39085, #26015, #138732, #92126 ),
 .UNSPECIFIED., .F., .F.,
 ( 4, 4 ),
 ( 0.0001555421464865875856, 0.0001737658007497212376 ),
 .UNSPECIFIED. ) ;
#127726=EDGE_CURVE ( 'NONE', #148041, #4447, #154549, .T. ) ;
#127767=CYLINDRICAL_SURFACE ( 'NONE', #62039, 1.000000000000000222 ) ;
#128302=CARTESIAN_POINT ( 'NONE',  ( 1.214306433183764966E-14, 2.428612866367529932E-14, 1.500000000000001332 ) ) ;
#128495=CARTESIAN_POINT ( 'NONE',  ( -2.659371061294795613, 0.4155010417826092151, -0.1333820918543257572 ) ) ;
#128922=VECTOR ( 'NONE', #21689, 1000.000000000000000 ) ;
#129327=ORIENTED_EDGE ( 'NONE', *, *, #17510, .T. ) ;
#129968=CARTESIAN_POINT ( 'NONE',  ( 2.000000000000011990, 2.453105802350476962E-14, 1.500000000000001332 ) ) ;
#130123=DIRECTION ( 'NONE',  ( -8.638326563840814399E-31, -0.000000000000000000, -1.000000000000000000 ) ) ;
#130225=CARTESIAN_POINT ( 'NONE',  ( 2.659371061294801386, -0.4155010417826092151, -0.1333820918543257850 ) ) ;
#130703=DIRECTION ( 'NONE',  ( 1.000000000000000000, 1.725633230170963762E-31, 8.638326563840814399E-31 ) ) ;
#130887=CARTESIAN_POINT ( 'NONE',  ( -1.651451222920911732, 0.8386022738108426244, 1.021479198850123060 ) ) ;
#130899=CARTESIAN_POINT ( 'NONE',  ( 2.325000000000003730, 0.05106627235655090274, -0.4999999999999941713 ) ) ;
#131352=CARTESIAN_POINT ( 'NONE',  ( -2.609770642201835855, -0.3830433331901521576, 0.000000000000000000 ) ) ;
#131368=ORIENTED_EDGE ( 'NONE', *, *, #27912, .T. ) ;
#131391=ORIENTED_EDGE ( 'NONE', *, *, #94915, .F. ) ;
#131490=DIRECTION ( 'NONE',  ( 8.638326563840809144E-31, 5.962633348652903386E-61, -1.000000000000000000 ) ) ;
#131752=( NAMED_UNIT ( * ) PLANE_ANGLE_UNIT ( ) SI_UNIT ( $, .RADIAN. ) );
#131938=CARTESIAN_POINT ( 'NONE',  ( 2.370092853298483959, 0.1904551827020779520, -0.4476525039842664810 ) ) ;
#132002=DIRECTION ( 'NONE',  ( 0.000000000000000000, 0.000000000000000000, 1.000000000000000000 ) ) ;
#132348=CARTESIAN_POINT ( 'NONE',  ( 2.680963302754415079, 0.4788041664859938318, -0.1016165050511480955 ) ) ;
#132350=AXIS2_PLACEMENT_3D ( 'NONE', #152629, #3149, #115927 ) ;
#132805=PRESENTATION_STYLE_ASSIGNMENT (( #592 ) ) ;
#133104=VERTEX_POINT ( 'NONE', #144435 ) ;
#133847=ORIENTED_EDGE ( 'NONE', *, *, #5366, .F. ) ;
#134057=VERTEX_POINT ( 'NONE', #164932 ) ;
#134448=FACE_OUTER_BOUND ( 'NONE', #105216, .T. ) ;
#134614=CARTESIAN_POINT ( 'NONE',  ( 1.214306433183764966E-14, 2.428612866367529932E-14, 1.500000000000001332 ) ) ;
#134739=DIRECTION ( 'NONE',  ( 1.000000000000000000, 0.000000000000000000, 8.638326563840826660E-31 ) ) ;
#134920=B_SPLINE_CURVE_WITH_KNOTS ( 'NONE', 3,
 ( #126536, #142737, #208746, #28953, #144877, #78752, #60373, #192498 ),
 .UNSPECIFIED., .F., .F.,
 ( 4, 2, 2, 4 ),
 ( 0.0007320770841321901784, 0.0008843033762534650366, 0.001036529668374739678, 0.001340982252617288527 ),
 .UNSPECIFIED. ) ;
#135562=CARTESIAN_POINT ( 'NONE',  ( -1.491410138560268495, -1.333748936243116745, 1.500000000000001332 ) ) ;
#135840=FILL_AREA_STYLE_COLOUR ( '', #15590 ) ;
#135951=ORIENTED_EDGE ( 'NONE', *, *, #55163, .F. ) ;
#135995=CARTESIAN_POINT ( 'NONE',  ( -2.324999999999998845, 0.000000000000000000, -0.5000000000000004441 ) ) ;
#136626=CARTESIAN_POINT ( 'NONE',  ( -1.600055350837869428, 1.204204895297060096, 1.480038727545138766 ) ) ;
#136925=FILL_AREA_STYLE_COLOUR ( '', #185582 ) ;
#136934=FACE_OUTER_BOUND ( 'NONE', #24099, .T. ) ;
#137030=ORIENTED_EDGE ( 'NONE', *, *, #166683, .T. ) ;
#137497=CARTESIAN_POINT ( 'NONE',  ( 1.452583904633400591, 1.374772708486753370, 1.500000000000001332 ) ) ;
#137887=UNCERTAINTY_MEASURE_WITH_UNIT (LENGTH_MEASURE( 1.000000000000000082E-05 ), #198809, 'distance_accuracy_value', 'NONE');
#138117=( NAMED_UNIT ( * ) PLANE_ANGLE_UNIT ( ) SI_UNIT ( $, .RADIAN. ) );
#138303=CARTESIAN_POINT ( 'NONE',  ( 1.532410409194677081, -1.041802156240267951, 1.385306760018462313 ) ) ;
#138306=DIRECTION ( 'NONE',  ( 8.638326563840814399E-31, 0.000000000000000000, 1.000000000000000000 ) ) ;
#138732=CARTESIAN_POINT ( 'NONE',  ( -2.680403734648525216, 0.4910177078054965838, -0.09999999999832666353 ) ) ;
#138759=AXIS2_PLACEMENT_3D ( 'NONE', #32406, #33463, #149353 ) ;
#138769=VERTEX_POINT ( 'NONE', #87171 ) ;
#138904=B_SPLINE_CURVE_WITH_KNOTS ( 'NONE', 3,
 ( #188540, #156051, #205851, #123643 ),
 .UNSPECIFIED., .F., .F.,
 ( 4, 4 ),
 ( 0.000000000000000000, 1.835777882413431832E-05 ),
 .UNSPECIFIED. ) ;
#138907=CARTESIAN_POINT ( 'NONE',  ( -2.681339180781858289, -0.4790681834518588644, -0.1012129971987970750 ) ) ;
#138920=ORIENTED_EDGE ( 'NONE', *, *, #164541, .F. ) ;
#139608=DIRECTION ( 'NONE',  ( -8.638326563840814399E-31, 0.000000000000000000, -1.000000000000000000 ) ) ;
#139680=( LENGTH_UNIT ( ) NAMED_UNIT ( * ) SI_UNIT ( .MILLI., .METRE. ) );
#139705=CARTESIAN_POINT ( 'NONE',  ( -1.715332513650474455, -0.7127186716553509660, 0.8729729531562419043 ) ) ;
#139778=ORIENTED_EDGE ( 'NONE', *, *, #124029, .T. ) ;
#140060=VECTOR ( 'NONE', #130123, 1000.000000000000000 ) ;
#140120=ADVANCED_FACE ( 'NONE', ( #205241 ), #90466, .T. ) ;
#140212=CARTESIAN_POINT ( 'NONE',  ( 1.607015867998825343, 0.9165151389911689872, 1.199999999999999734 ) ) ;
#140937=VERTEX_POINT ( 'NONE', #143651 ) ;
#141019=PRESENTATION_STYLE_ASSIGNMENT (( #207027 ) ) ;
#141335=FACE_BOUND ( 'NONE', #1779, .T. ) ;
#141632=CARTESIAN_POINT ( 'NONE',  ( -1.404019654740992440, 1.209281689291645367, 1.481605035838516216 ) ) ;
#141799=CARTESIAN_POINT ( 'NONE',  ( 1.580854408705430370, 0.9623865910009720137, 1.305104700536227957 ) ) ;
#142031=EDGE_LOOP ( 'NONE', ( #88692, #65591, #131391, #54429 ) ) ;
#142391=CARTESIAN_POINT ( 'NONE',  ( 0.000000000000000000, 0.000000000000000000, 0.000000000000000000 ) ) ;
#142689=CARTESIAN_POINT ( 'NONE',  ( -1.607015867998815128, 0.9165151389911810886, 1.199999999999999734 ) ) ;
#142737=CARTESIAN_POINT ( 'NONE',  ( -2.324999999999999289, -0.05106627235655240848, -0.5000000000000004441 ) ) ;
#142892=DIRECTION ( 'NONE',  ( -8.638326563840814399E-31, 0.000000000000000000, -1.000000000000000000 ) ) ;
#143465=DIRECTION ( 'NONE',  ( -1.000000000000000000, -3.451266460341926649E-31, -8.638326563840809144E-31 ) ) ;
#143646=ORIENTED_EDGE ( 'NONE', *, *, #89086, .F. ) ;
#143651=CARTESIAN_POINT ( 'NONE',  ( 2.325000000000005063, 0.000000000000000000, -0.5000000000000004441 ) ) ;
#143679=VECTOR ( 'NONE', #139608, 1000.000000000000000 ) ;
#143924=AXIS2_PLACEMENT_3D ( 'NONE', #198575, #2498, #118483 ) ;
#143964=DIRECTION ( 'NONE',  ( 8.638326563840814399E-31, 0.000000000000000000, 1.000000000000000000 ) ) ;
#144316=CARTESIAN_POINT ( 'NONE',  ( 2.679285714285720044, -0.4970443252110337551, -0.09999999999999592548 ) ) ;
#144435=CARTESIAN_POINT ( 'NONE',  ( -1.452583904633382383, 1.374772708486763806, 1.500000000000001332 ) ) ;
#144877=CARTESIAN_POINT ( 'NONE',  ( -2.393960638069832836, -0.2282907053230411043, -0.4203461706283347921 ) ) ;
#145082=CARTESIAN_POINT ( 'NONE',  ( -2.335253425310764186, 0.1017894593877472081, -0.4879271257269361395 ) ) ;
#145372=CARTESIAN_POINT ( 'NONE',  ( -2.580963302752292243, -0.4788041664876945269, 0.000000000000000000 ) ) ;
#145815=PRODUCT_DEFINITION_SHAPE ( 'NONE', 'NONE',  #51771 ) ;
#145834=AXIS2_PLACEMENT_3D ( 'NONE', #213719, #131490, #143465 ) ;
#146336=EDGE_LOOP ( 'NONE', ( #172661, #9388, #160346, #124628 ) ) ;
#146443=VERTEX_POINT ( 'NONE', #9422 ) ;
#146474=ADVANCED_FACE ( 'NONE', ( #171929 ), #122202, .F. ) ;
#146813=CARTESIAN_POINT ( 'NONE',  ( -2.642331537210447667, 0.3998488639457564719, -0.1525862845480549512 ) ) ;
#146852=LINE ( 'NONE', #77550, #148895 ) ;
#147052=( GEOMETRIC_REPRESENTATION_CONTEXT ( 3 ) GLOBAL_UNCERTAINTY_ASSIGNED_CONTEXT ( ( #97359 ) ) GLOBAL_UNIT_ASSIGNED_CONTEXT ( ( #56717, #104406, #4722 ) ) REPRESENTATION_CONTEXT ( 'NONE', 'WORKASPACE' ) );
#147215=DIRECTION ( 'NONE',  ( -8.638326563840814399E-31, 0.000000000000000000, -1.000000000000000000 ) ) ;
#147362=AXIS2_PLACEMENT_3D ( 'NONE', #24356, #57948, #156533 ) ;
#147441=EDGE_CURVE ( 'NONE', #174147, #106354, #183954, .T. ) ;
#147580=STYLED_ITEM ( 'NONE', ( #207237 ), #16748 ) ;
#147597=ORIENTED_EDGE ( 'NONE', *, *, #64524, .T. ) ;
#147868=B_SPLINE_CURVE_WITH_KNOTS ( 'NONE', 3,
 ( #155708, #122229, #141632, #207640, #59258, #142689 ),
 .UNSPECIFIED., .F., .F.,
 ( 4, 2, 4 ),
 ( 0.000000000000000000, 0.0003472644472073818721, 0.0006945288944147637441 ),
 .UNSPECIFIED. ) ;
#147901=DIRECTION ( 'NONE',  ( -8.638326563840814399E-31, -0.000000000000000000, -1.000000000000000000 ) ) ;
#147972=( LENGTH_UNIT ( ) NAMED_UNIT ( * ) SI_UNIT ( .MILLI., .METRE. ) );
#148021=ORIENTED_EDGE ( 'NONE', *, *, #71393, .F. ) ;
#148041=VERTEX_POINT ( 'NONE', #73400 ) ;
#148610=CARTESIAN_POINT ( 'NONE',  ( 2.474627113408591761, -0.3228523939998609871, -0.3300564308867471319 ) ) ;
#148787=FACE_OUTER_BOUND ( 'NONE', #53271, .T. ) ;
#148895=VECTOR ( 'NONE', #147901, 1000.000000000000000 ) ;
#148907=CARTESIAN_POINT ( 'NONE',  ( -2.680963302752293664, 0.4788041664877169534, -0.1016165050528608921 ) ) ;
#149017=SURFACE_STYLE_FILL_AREA ( #16863 ) ;
#149353=DIRECTION ( 'NONE',  ( 1.000000000000000000, 0.000000000000000000, 0.000000000000000000 ) ) ;
#149559=AXIS2_PLACEMENT_3D ( 'NONE', #172952, #90639, #156699 ) ;
#149674=CARTESIAN_POINT ( 'NONE',  ( -5.249999999999987566, 0.000000000000000000, 1.599999999999997202 ) ) ;
#149946=AXIS2_PLACEMENT_3D ( 'NONE', #145372, #80317, #65111 ) ;
#150221=EDGE_CURVE ( 'NONE', #33663, #105242, #23141, .T. ) ;
#150577=CARTESIAN_POINT ( 'NONE',  ( -5.249999999999987566, 1.374772708486751593, 1.000000000000000888 ) ) ;
#150758=CARTESIAN_POINT ( 'NONE',  ( -1.992392395334928734, -0.1979219324388414303, 0.6149939648489994859 ) ) ;
#150777=CARTESIAN_POINT ( 'NONE',  ( 2.000000000000011990, 2.453103989352373237E-14, 0.5999999999999970912 ) ) ;
#150897=ORIENTED_EDGE ( 'NONE', *, *, #200985, .F. ) ;
#151017=MECHANICAL_DESIGN_GEOMETRIC_PRESENTATION_REPRESENTATION('',(#178682),#57611);
#151281=DIRECTION ( 'NONE',  ( -8.638326563840814399E-31, 0.000000000000000000, -1.000000000000000000 ) ) ;
#151313=DIRECTION ( 'NONE',  ( -8.638326563840814399E-31, 0.000000000000000000, -1.000000000000000000 ) ) ;
#151801=CARTESIAN_POINT ( 'NONE',  ( 2.680963302752298993, 0.4788041664877049075, -8.638326563840814180E-32 ) ) ;
#152613=VERTEX_POINT ( 'NONE', #119412 ) ;
#152629=CARTESIAN_POINT ( 'NONE',  ( 0.000000000000000000, 0.000000000000000000, -0.5000000000000004441 ) ) ;
#152640=CARTESIAN_POINT ( 'NONE',  ( 1.214306433183764966E-14, 2.428612866367529932E-14, 1.500000000000001332 ) ) ;
#152812=EDGE_LOOP ( 'NONE', ( #126531, #107702, #32949, #80468, #147597, #63031, #43294, #113788 ) ) ;
#152954=CARTESIAN_POINT ( 'NONE',  ( -5.249999999999987566, -1.374772708486751593, 1.000000000000000888 ) ) ;
#153043=CARTESIAN_POINT ( 'NONE',  ( 2.609770642201841184, 0.3830433331901660354, -0.1872689674646474400 ) ) ;
#153216=DIRECTION ( 'NONE',  ( 1.000000000000000000, 3.451266460341926649E-31, 8.638326563840810896E-31 ) ) ;
#153925=B_SPLINE_CURVE_WITH_KNOTS ( 'NONE', 3,
 ( #132348, #85685, #20665, #182105, #168007, #33734, #51062, #2271, #52129, #99812, #65152, #35866, #185305, #36928, #17464, #103011 ),
 .UNSPECIFIED., .F., .F.,
 ( 4, 3, 3, 3, 3, 4 ),
 ( 1.835777882413431832E-05, 2.688023894040715345E-05, 5.355394816894561410E-05, 9.073944566320893250E-05, 0.0001419156937261367561, 0.0001738851243175512954 ),
 .UNSPECIFIED. ) ;
#153937=CARTESIAN_POINT ( 'NONE',  ( -1.754755943840817123, 0.9608980427861949503, 1.301694008101299538 ) ) ;
#153940=CARTESIAN_POINT ( 'NONE',  ( -1.596166908135297824, -1.206333752204373555, 1.472837400516048723 ) ) ;
#153991=ORIENTED_EDGE ( 'NONE', *, *, #43201, .F. ) ;
#154242=ADVANCED_FACE ( 'NONE', ( #159866 ), #11468, .F. ) ;
#154305=EDGE_CURVE ( 'NONE', #111709, #88893, #25584, .T. ) ;
#154439=CARTESIAN_POINT ( 'NONE',  ( 1.214306433183764966E-14, 2.428612866367529932E-14, 1.500000000000001332 ) ) ;
#154549=CIRCLE ( 'NONE', #119977, 0.09999999999999982514 ) ;
#154696=CARTESIAN_POINT ( 'NONE',  ( 2.609770642201841184, -0.3830433331901555993, 0.000000000000000000 ) ) ;
#154756=EDGE_LOOP ( 'NONE', ( #16740, #98801, #158397, #20998 ) ) ;
#155145=CARTESIAN_POINT ( 'NONE',  ( -2.666414593264807120, -0.4259009368094196502, -0.1247943508829715553 ) ) ;
#155400=VECTOR ( 'NONE', #143964, 1000.000000000000000 ) ;
#155604=( GEOMETRIC_REPRESENTATION_CONTEXT ( 3 ) GLOBAL_UNCERTAINTY_ASSIGNED_CONTEXT ( ( #182605 ) ) GLOBAL_UNIT_ASSIGNED_CONTEXT ( ( #147972, #131752, #17923 ) ) REPRESENTATION_CONTEXT ( 'NONE', 'WORKASPACE' ) );
#155682=DIRECTION ( 'NONE',  ( -8.638326563840814399E-31, 0.000000000000000000, -1.000000000000000000 ) ) ;
#155708=CARTESIAN_POINT ( 'NONE',  ( -1.237941840313982578, 1.374772708486763806, 1.500000000000001332 ) ) ;
#155863=CARTESIAN_POINT ( 'NONE',  ( 0.000000000000000000, 0.000000000000000000, -5.732590180780448463 ) ) ;
#155936=CARTESIAN_POINT ( 'NONE',  ( -1.815167269671988270, -0.3943365573012030945, 0.6613654005181992535 ) ) ;
#156051=CARTESIAN_POINT ( 'NONE',  ( 2.680403734646828351, 0.4910177078051911614, -0.09999999999999592548 ) ) ;
#156067=CIRCLE ( 'NONE', #138759, 2.000000000000000000 ) ;
#156075=CARTESIAN_POINT ( 'NONE',  ( -1.777638883463123598, -0.9165151389911724289, 1.199999999999999734 ) ) ;
#156117=VERTEX_POINT ( 'NONE', #191249 ) ;
#156171=FACE_OUTER_BOUND ( 'NONE', #197356, .T. ) ;
#156533=DIRECTION ( 'NONE',  ( -1.000000000000000000, 0.000000000000000000, -8.638326563840826660E-31 ) ) ;
#156699=DIRECTION ( 'NONE',  ( -1.000000000000000000, -3.451266460341927087E-31, -8.638326563840810896E-31 ) ) ;
#156816=ORIENTED_EDGE ( 'NONE', *, *, #18383, .T. ) ;
#156987=DIRECTION ( 'NONE',  ( -1.000000000000000000, -3.451266460341925773E-31, -8.638326563840809144E-31 ) ) ;
#157185=CARTESIAN_POINT ( 'NONE',  ( -1.324887192667531632, -1.296481010641094000, 1.500000000000001776 ) ) ;
#157239=( NAMED_UNIT ( * ) SI_UNIT ( $, .STERADIAN. ) SOLID_ANGLE_UNIT ( ) );
#157448=SURFACE_STYLE_USAGE ( .BOTH. , #25287 ) ;
#157786=CARTESIAN_POINT ( 'NONE',  ( 1.777638883463123598, -0.9165151389911446733, 1.199999999999999734 ) ) ;
#157979=ADVANCED_FACE ( 'NONE', ( #208893 ), #127767, .F. ) ;
#158054=( NAMED_UNIT ( * ) SI_UNIT ( $, .STERADIAN. ) SOLID_ANGLE_UNIT ( ) );
#158080=EDGE_CURVE ( 'NONE', #110706, #10766, #113618, .T. ) ;
#158397=ORIENTED_EDGE ( 'NONE', *, *, #50862, .T. ) ;
#158600=FACE_OUTER_BOUND ( 'NONE', #115146, .T. ) ;
#158611=DIRECTION ( 'NONE',  ( 8.638326563840809144E-31, 5.962633348652903386E-61, -1.000000000000000000 ) ) ;
#158802=DIRECTION ( 'NONE',  ( 0.000000000000000000, 0.000000000000000000, -1.000000000000000000 ) ) ;
#159435=CARTESIAN_POINT ( 'NONE',  ( 0.000000000000000000, 0.000000000000000000, 0.000000000000000000 ) ) ;
#159443=CARTESIAN_POINT ( 'NONE',  ( 2.665936209291948078, -0.4260822056534815938, -0.1252292841820018543 ) ) ;
#159866=FACE_OUTER_BOUND ( 'NONE', #191334, .T. ) ;
#160346=ORIENTED_EDGE ( 'NONE', *, *, #55794, .F. ) ;
#160513=CARTESIAN_POINT ( 'NONE',  ( 2.632325991586431435, -0.3920720250259056017, -0.1636427795756393855 ) ) ;
#160705=PLANE ( 'NONE',  #94759 ) ;
#160821=ORIENTED_EDGE ( 'NONE', *, *, #40961, .T. ) ;
#161266=DIRECTION ( 'NONE',  ( 1.000000000000000000, 0.000000000000000000, 0.000000000000000000 ) ) ;
#161298=CARTESIAN_POINT ( 'NONE',  ( -2.370002892456521959, 0.1903694832692625627, -0.4477549104883318254 ) ) ;
#161613=EDGE_LOOP ( 'NONE', ( #180528, #83258, #91703, #36212 ) ) ;
#161825=AXIS2_PLACEMENT_3D ( 'NONE', #88219, #188909, #153216 ) ;
#161984=CARTESIAN_POINT ( 'NONE',  ( -2.680951471028987232, 0.4698187958462037295, -0.1032074697909404620 ) ) ;
#162210=AXIS2_PLACEMENT_3D ( 'NONE', #149674, #166995, #1255 ) ;
#162523=VERTEX_POINT ( 'NONE', #86386 ) ;
#162693=ORIENTED_EDGE ( 'NONE', *, *, #199649, .T. ) ;
#162781=DIRECTION ( 'NONE',  ( 1.000000000000000000, 1.725633230170963762E-31, 8.638326563840814399E-31 ) ) ;
#162792=ORIENTED_EDGE ( 'NONE', *, *, #89086, .T. ) ;
#163028=PRODUCT_DEFINITION_FORMATION_WITH_SPECIFIED_SOURCE ( 'ANY', '', #107661, .NOT_KNOWN. ) ;
#163470=ORIENTED_EDGE ( 'NONE', *, *, #5768, .F. ) ;
#163566=CARTESIAN_POINT ( 'NONE',  ( 2.679285714285720044, -0.4970443252110337551, 0.000000000000000000 ) ) ;
#163587=ORIENTED_EDGE ( 'NONE', *, *, #97862, .F. ) ;
#164030=CARTESIAN_POINT ( 'NONE',  ( 1.712858683735189347, 1.037413707456548373, 1.381497717048131513 ) ) ;
#164270=ADVANCED_FACE ( 'NONE', ( #136934 ), #170476, .T. ) ;
#164389=CARTESIAN_POINT ( 'NONE',  ( -1.850000000000000089, 0.09855238430052820631, 0.5999999999999969802 ) ) ;
#164401=CARTESIAN_POINT ( 'NONE',  ( 2.609770642201841184, 0.3830433331901660354, -0.1872689674646474400 ) ) ;
#164541=EDGE_CURVE ( 'NONE', #162523, #31095, #68159, .T. ) ;
#164683=SURFACE_SIDE_STYLE ('',( #98622 ) ) ;
#164932=CARTESIAN_POINT ( 'NONE',  ( -2.679285714285713826, -0.4970443252110337551, 0.000000000000000000 ) ) ;
#165268=FILL_AREA_STYLE_COLOUR ( '', #96882 ) ;
#165943=CYLINDRICAL_SURFACE ( 'NONE', #78619, 0.09999999999999982514 ) ;
#166278=B_SPLINE_CURVE_WITH_KNOTS ( 'NONE', 3,
 ( #195457, #96910, #61180, #65415, #211678, #164030, #30834, #63314 ),
 .UNSPECIFIED., .F., .F.,
 ( 4, 2, 2, 4 ),
 ( 0.000000000000000000, 0.0001671579969091590092, 0.0003343159938183180185, 0.0006686319876366360370 ),
 .UNSPECIFIED. ) ;
#166307=EDGE_LOOP ( 'NONE', ( #212350, #163587, #184065, #6073, #76864, #169847, #2218, #103636 ) ) ;
#166428=CARTESIAN_POINT ( 'NONE',  ( 2.725000000000005862, 0.000000000000000000, 0.000000000000000000 ) ) ;
#166683=EDGE_CURVE ( 'NONE', #106354, #15498, #190783, .T. ) ;
#166982=AXIS2_PLACEMENT_3D ( 'NONE', #152954, #4529, #86887 ) ;
#166995=DIRECTION ( 'NONE',  ( 1.000000000000000000, 1.725633230170963762E-31, 8.638326563840814399E-31 ) ) ;
#167000=CARTESIAN_POINT ( 'NONE',  ( -1.945152801660234188, -0.4725272983825999917, 0.7134944055886121017 ) ) ;
#167017=DIRECTION ( 'NONE',  ( 1.000000000000000000, 0.000000000000000000, 8.638326563840826660E-31 ) ) ;
#167100=CIRCLE ( 'NONE', #73704, 2.324999999999998845 ) ;
#167215=DIRECTION ( 'NONE',  ( 8.638326563840814399E-31, 0.000000000000000000, 1.000000000000000000 ) ) ;
#167295=ORIENTED_EDGE ( 'NONE', *, *, #29276, .T. ) ;
#167565=VERTEX_POINT ( 'NONE', #148907 ) ;
#168007=CARTESIAN_POINT ( 'NONE',  ( 2.679885790744704899, 0.4618020869172074216, -0.1056289066552755923 ) ) ;
#168052=FACE_OUTER_BOUND ( 'NONE', #49518, .T. ) ;
#168097=DIRECTION ( 'NONE',  ( 8.638326563840814399E-31, -0.000000000000000000, 1.000000000000000000 ) ) ;
#168668=ORIENTED_EDGE ( 'NONE', *, *, #111248, .T. ) ;
#168856=ORIENTED_EDGE ( 'NONE', *, *, #158080, .T. ) ;
#168999=ORIENTED_EDGE ( 'NONE', *, *, #187563, .T. ) ;
#169097=EDGE_CURVE ( 'NONE', #134057, #89282, #146852, .T. ) ;
#169141=B_SPLINE_CURVE_WITH_KNOTS ( 'NONE', 3,
 ( #196138, #97585, #45633, #116001, #32557, #96528 ),
 .UNSPECIFIED., .F., .F.,
 ( 4, 2, 4 ),
 ( 0.001490700410107441247, 0.002078801942328945690, 0.002666903474550449699 ),
 .UNSPECIFIED. ) ;
#169209=DIRECTION ( 'NONE',  ( -8.638326563840814399E-31, 0.000000000000000000, -1.000000000000000000 ) ) ;
#169649=DIRECTION ( 'NONE',  ( -1.000000000000000000, -3.451266460341925773E-31, -8.638326563840809144E-31 ) ) ;
#169847=ORIENTED_EDGE ( 'NONE', *, *, #117853, .T. ) ;
#170354=DIRECTION ( 'NONE',  ( 1.000000000000000000, 1.725633230170963762E-31, 8.638326563840814399E-31 ) ) ;
#170447=EDGE_CURVE ( 'NONE', #156117, #182073, #29847, .T. ) ;
#170476=CYLINDRICAL_SURFACE ( 'NONE', #204376, 0.09999999999999982514 ) ;
#171149=VERTEX_POINT ( 'NONE', #53539 ) ;
#171339=DIRECTION ( 'NONE',  ( 1.000000000000000000, 0.000000000000000000, 0.000000000000000000 ) ) ;
#171348=ADVANCED_FACE ( 'NONE', ( #35140 ), #1560, .F. ) ;
#171541=VERTEX_POINT ( 'NONE', #205105 ) ;
#171548=AXIS2_PLACEMENT_3D ( 'NONE', #182373, #167215, #134739 ) ;
#171745=DIRECTION ( 'NONE',  ( -8.638326563840809144E-31, -5.962633348652903386E-61, 1.000000000000000000 ) ) ;
#171868=LINE ( 'NONE', #41896, #980 ) ;
#171929=FACE_OUTER_BOUND ( 'NONE', #106901, .T. ) ;
#172190=CARTESIAN_POINT ( 'NONE',  ( -1.850000000000000089, 2.265195232789710231E-16, 0.5999999999999969802 ) ) ;
#172450=ORIENTED_EDGE ( 'NONE', *, *, #147441, .F. ) ;
#172612=FILL_AREA_STYLE ('',( #135840 ) ) ;
#172646=ORIENTED_EDGE ( 'NONE', *, *, #118767, .T. ) ;
#172661=ORIENTED_EDGE ( 'NONE', *, *, #87337, .F. ) ;
#172666=ORIENTED_EDGE ( 'NONE', *, *, #96386, .T. ) ;
#172818=ORIENTED_EDGE ( 'NONE', *, *, #87041, .T. ) ;
#172833=B_SPLINE_CURVE_WITH_KNOTS ( 'NONE', 3,
 ( #150777, #54331, #35930, #199484, #51130, #117252 ),
 .UNSPECIFIED., .F., .F.,
 ( 4, 2, 4 ),
 ( 0.001490700410107413275, 0.002078801942328931812, 0.002666903474550450567 ),
 .UNSPECIFIED. ) ;
#172838=ADVANCED_FACE ( 'NONE', ( #81617 ), #113127, .F. ) ;
#172952=CARTESIAN_POINT ( 'NONE',  ( 0.000000000000000000, 0.000000000000000000, 0.000000000000000000 ) ) ;
#173447=CARTESIAN_POINT ( 'NONE',  ( -1.403658749385957139, -1.209764585679680593, 1.481909061747194167 ) ) ;
#173591=DIRECTION ( 'NONE',  ( -1.000000000000000000, -3.451266460341926211E-31, -8.638326563840810896E-31 ) ) ;
#173667=LINE ( 'NONE', #46860, #69902 ) ;
#174015=CIRCLE ( 'NONE', #177393, 1.850000000000000089 ) ;
#174026=FACE_OUTER_BOUND ( 'NONE', #206730, .T. ) ;
#174147=VERTEX_POINT ( 'NONE', #64667 ) ;
#174280=CARTESIAN_POINT ( 'NONE',  ( 1.607015867998825343, 0.9165151389911689872, 1.199999999999999734 ) ) ;
#174360=DIRECTION ( 'NONE',  ( -1.000000000000000000, -3.451266460341925773E-31, -8.638326563840809144E-31 ) ) ;
#174687=DIRECTION ( 'NONE',  ( 1.000000000000000000, 3.451266460341927087E-31, 0.000000000000000000 ) ) ;
#174774=FACE_OUTER_BOUND ( 'NONE', #142031, .T. ) ;
#174794=ORIENTED_EDGE ( 'NONE', *, *, #199649, .F. ) ;
#175068=DIRECTION ( 'NONE',  ( 1.000000000000000000, 1.725633230170963762E-31, 8.638326563840814399E-31 ) ) ;
#175370=CARTESIAN_POINT ( 'NONE',  ( -2.725000000000000089, 0.000000000000000000, 0.000000000000000000 ) ) ;
#175789=AXIS2_PLACEMENT_3D ( 'NONE', #126382, #175068, #158802 ) ;
#175834=DIRECTION ( 'NONE',  ( -1.000000000000000000, 0.000000000000000000, -8.638326563840826660E-31 ) ) ;
#175841=CARTESIAN_POINT ( 'NONE',  ( 1.849999999999999867, 0.1967728318288075040, 0.5999999999999968692 ) ) ;
#176425=CARTESIAN_POINT ( 'NONE',  ( -5.249999999999987566, 0.000000000000000000, 1.599999999999997202 ) ) ;
#176755=FACE_OUTER_BOUND ( 'NONE', #18439, .T. ) ;
#177196=ADVANCED_FACE ( 'NONE', ( #156171 ), #187577, .T. ) ;
#177393=AXIS2_PLACEMENT_3D ( 'NONE', #152640, #202427, #181926 ) ;
#177546=CARTESIAN_POINT ( 'NONE',  ( -1.850000000000000089, 2.265195232789710231E-16, 0.5999999999999969802 ) ) ;
#177547=VECTOR ( 'NONE', #54800, 1000.000000000000000 ) ;
#177803=B_SPLINE_CURVE_WITH_KNOTS ( 'NONE', 3,
 ( #34337, #198952, #17007, #739, #118860, #100412, #49530, #115654 ),
 .UNSPECIFIED., .F., .F.,
 ( 4, 2, 2, 4 ),
 ( 0.0003136881264510900055, 0.0009048594355810645352, 0.001200445090146051936, 0.001496030744711039119 ),
 .UNSPECIFIED. ) ;
#177926=CIRCLE ( 'NONE', #25755, 1.850000000000000089 ) ;
#177933=AXIS2_PLACEMENT_3D ( 'NONE', #180625, #771, #50627 ) ;
#177961=DIRECTION ( 'NONE',  ( 8.638326563840814399E-31, -0.000000000000000000, 1.000000000000000000 ) ) ;
#178080=B_SPLINE_CURVE_WITH_KNOTS ( 'NONE', 3,
 ( #111839, #178912, #160513, #61950, #59811, #130225, #159443, #112901, #125966, #12116, #179969, #9985, #44649, #46787, #113972, #144316 ),
 .UNSPECIFIED., .F., .F.,
 ( 4, 3, 3, 3, 3, 4 ),
 ( 5.987702205360377997E-19, 5.045320844149813800E-05, 9.514731479431012807E-05, 0.0001285019506257865799, 0.0001554096905453329267, 0.0001737658007497178494 ),
 .UNSPECIFIED. ) ;
#178233=VECTOR ( 'NONE', #8333, 1000.000000000000000 ) ;
#178682=STYLED_ITEM ( 'NONE', ( #94128 ), #197875 ) ;
#178835=ADVANCED_FACE ( 'NONE', ( #158600 ), #46080, .T. ) ;
#178912=CARTESIAN_POINT ( 'NONE',  ( 2.621219598810454965, -0.3864874759363098877, -0.1754412237054647494 ) ) ;
#178994=CARTESIAN_POINT ( 'NONE',  ( -1.999999999999988010, -0.09816220177715248574, 0.5999999999999945377 ) ) ;
#179299=CARTESIAN_POINT ( 'NONE',  ( -2.680963302752292332, 0.4787599428022954462, -0.1016242801182818956 ) ) ;
#179393=EDGE_CURVE ( 'NONE', #162523, #174147, #25171, .T. ) ;
#179634=EDGE_CURVE ( 'NONE', #62251, #110706, #178080, .T. ) ;
#179969=CARTESIAN_POINT ( 'NONE',  ( 2.679728069698092074, -0.4610709815545778190, -0.1059060488087510826 ) ) ;
#180351=CARTESIAN_POINT ( 'NONE',  ( -2.651186565980338639, 0.4067314603539678441, -0.1428011528578489453 ) ) ;
#180528=ORIENTED_EDGE ( 'NONE', *, *, #124029, .F. ) ;
#180625=CARTESIAN_POINT ( 'NONE',  ( 2.580963302752299349, 0.4788041664877049075, 0.000000000000000000 ) ) ;
#180878=COLOUR_RGB ( '', 0.66274510, 0.83137255, 0.94901961) ;
#180925=FACE_OUTER_BOUND ( 'NONE', #75895, .T. ) ;
#181039=ORIENTED_EDGE ( 'NONE', *, *, #65677, .F. ) ;
#181359=CIRCLE ( 'NONE', #11892, 2.725000000000000089 ) ;
#181482=AXIS2_PLACEMENT_3D ( 'NONE', #205407, #26668, #92772 ) ;
#181926=DIRECTION ( 'NONE',  ( 1.000000000000000000, 0.000000000000000000, 0.000000000000000000 ) ) ;
#182073=VERTEX_POINT ( 'NONE', #84835 ) ;
#182105=CARTESIAN_POINT ( 'NONE',  ( 2.680610894905853137, 0.4704162359921160164, -0.1034257855107231783 ) ) ;
#182196=EDGE_CURVE ( 'NONE', #10112, #171541, #56552, .T. ) ;
#182209=ORIENTED_EDGE ( 'NONE', *, *, #154305, .T. ) ;
#182373=CARTESIAN_POINT ( 'NONE',  ( 2.580963302752299349, 0.4788041664877049075, 0.000000000000000000 ) ) ;
#182391=ADVANCED_FACE ( 'NONE', ( #176755 ), #212431, .T. ) ;
#182460=DIRECTION ( 'NONE',  ( -1.000000000000000000, -3.451266460341925773E-31, -8.638326563840809144E-31 ) ) ;
#182535=CONICAL_SURFACE ( 'NONE', #13095, 2.324999999999998845, 0.7853981633974461696 ) ;
#182605=UNCERTAINTY_MEASURE_WITH_UNIT (LENGTH_MEASURE( 1.000000000000000082E-05 ), #147972, 'distance_accuracy_value', 'NONE');
#182821=ORIENTED_EDGE ( 'NONE', *, *, #117712, .T. ) ;
#182976=VECTOR ( 'NONE', #107777, 1000.000000000000000 ) ;
#183212=CYLINDRICAL_SURFACE ( 'NONE', #110178, 2.000000000000000000 ) ;
#183645=SURFACE_SIDE_STYLE ('',( #149017 ) ) ;
#183807=EDGE_LOOP ( 'NONE', ( #8278, #86921, #116095, #201438 ) ) ;
#183954=LINE ( 'NONE', #129968, #33363 ) ;
#184065=ORIENTED_EDGE ( 'NONE', *, *, #9722, .T. ) ;
#184111=( NAMED_UNIT ( * ) PLANE_ANGLE_UNIT ( ) SI_UNIT ( $, .RADIAN. ) );
#184266=CARTESIAN_POINT ( 'NONE',  ( 1.214306433183764966E-14, 2.428612866367529932E-14, 1.500000000000001332 ) ) ;
#184493=B_SPLINE_CURVE_WITH_KNOTS ( 'NONE', 3,
 ( #174280, #141799, #206743, #207803, #56243, #188360 ),
 .UNSPECIFIED., .F., .F.,
 ( 4, 2, 4 ),
 ( 0.000000000000000000, 0.0003473417695167276627, 0.0006946835390334553254 ),
 .UNSPECIFIED. ) ;
#184614=EDGE_LOOP ( 'NONE', ( #153991, #52105, #126110, #10430 ) ) ;
#184823=EDGE_CURVE ( 'NONE', #146443, #35153, #98289, .T. ) ;
#185305=CARTESIAN_POINT ( 'NONE',  ( 2.630984769852976690, 0.3922140236936443869, -0.1649412225328064641 ) ) ;
#185348=CARTESIAN_POINT ( 'NONE',  ( -1.713667314260263419, 1.036161614632730377, 1.380621972511379081 ) ) ;
#185582=COLOUR_RGB ( '', 0.08235294, 0.09019608, 0.10196078) ;
#185629=SURFACE_SIDE_STYLE ('',( #119646 ) ) ;
#185934=DIRECTION ( 'NONE',  ( -1.000000000000000000, -3.451266460341927087E-31, 0.000000000000000000 ) ) ;
#186562=CARTESIAN_POINT ( 'NONE',  ( -2.680610894905847363, -0.4704162359921021386, -0.1034257855107231783 ) ) ;
#186701=CARTESIAN_POINT ( 'NONE',  ( 1.945152801660263719, 0.4725272983826271367, 0.7134944055886273118 ) ) ;
#187034=EDGE_CURVE ( 'NONE', #35153, #33663, #56843, .T. ) ;
#187316=( LENGTH_UNIT ( ) NAMED_UNIT ( * ) SI_UNIT ( .MILLI., .METRE. ) );
#187511=VERTEX_POINT ( 'NONE', #131352 ) ;
#187563=EDGE_CURVE ( 'NONE', #156117, #52075, #40314, .T. ) ;
#187577=CYLINDRICAL_SURFACE ( 'NONE', #166982, 0.5000000000000000000 ) ;
#187988=FACE_OUTER_BOUND ( 'NONE', #36936, .T. ) ;
#188092=CARTESIAN_POINT ( 'NONE',  ( 1.404019654741015755, -1.209281689291617834, 1.481605035838507334 ) ) ;
#188164=DIRECTION ( 'NONE',  ( -1.000000000000000000, -3.451266460341925773E-31, -8.638326563840809144E-31 ) ) ;
#188360=CARTESIAN_POINT ( 'NONE',  ( 1.237941840314000785, 1.374772708486753370, 1.500000000000001332 ) ) ;
#188486=DIRECTION ( 'NONE',  ( 1.000000000000000000, 3.451266460341927087E-31, 0.000000000000000000 ) ) ;
#188540=CARTESIAN_POINT ( 'NONE',  ( 2.679285714285720044, 0.4970443252110459120, -0.09999999999999592548 ) ) ;
#188883=APPLICATION_CONTEXT ( 'automotive_design' ) ;
#188909=DIRECTION ( 'NONE',  ( 8.638326563840814399E-31, 0.000000000000000000, 1.000000000000000000 ) ) ;
#188915=EDGE_CURVE ( 'NONE', #105242, #107614, #115973, .T. ) ;
#189308=ORIENTED_EDGE ( 'NONE', *, *, #117712, .F. ) ;
#189406=ORIENTED_EDGE ( 'NONE', *, *, #184823, .F. ) ;
#189458=ORIENTED_EDGE ( 'NONE', *, *, #108709, .T. ) ;
#189585=EDGE_CURVE ( 'NONE', #31095, #111709, #184493, .T. ) ;
#189930=EDGE_CURVE ( 'NONE', #88893, #133104, #88391, .T. ) ;
#189935=EDGE_CURVE ( 'NONE', #140937, #85328, #89020, .T. ) ;
#190086=ORIENTED_EDGE ( 'NONE', *, *, #97862, .T. ) ;
#190517=FACE_OUTER_BOUND ( 'NONE', #161613, .T. ) ;
#190606=CARTESIAN_POINT ( 'NONE',  ( 2.580963302752299349, 0.4788041664877049075, 0.000000000000000000 ) ) ;
#190657=CARTESIAN_POINT ( 'NONE',  ( -5.249999999999987566, 0.9165151389911689872, 1.199999999999999734 ) ) ;
#190783=CIRCLE ( 'NONE', #55975, 2.000000000000000000 ) ;
#190946=DIRECTION ( 'NONE',  ( 8.638326563840814399E-31, -0.000000000000000000, 1.000000000000000000 ) ) ;
#191249=CARTESIAN_POINT ( 'NONE',  ( -1.777638883463123598, -0.9165151389911724289, 1.199999999999999734 ) ) ;
#191334=EDGE_LOOP ( 'NONE', ( #194006, #44689, #102456, #181039 ) ) ;
#191433=DIRECTION ( 'NONE',  ( 1.000000000000000000, 3.451266460341926211E-31, 0.000000000000000000 ) ) ;
#191584=EDGE_CURVE ( 'NONE', #3254, #31095, #41935, .T. ) ;
#191630=VERTEX_POINT ( 'NONE', #40865 ) ;
#191907=ORIENTED_EDGE ( 'NONE', *, *, #158080, .F. ) ;
#191936=ORIENTED_EDGE ( 'NONE', *, *, #102584, .F. ) ;
#192149=PLANE ( 'NONE',  #205177 ) ;
#192369=ADVANCED_FACE ( 'NONE', ( #148787 ), #201771, .T. ) ;
#192498=CARTESIAN_POINT ( 'NONE',  ( -2.609770642201835855, -0.3830433331901521576, -0.1872689674646474400 ) ) ;
#192501=DIRECTION ( 'NONE',  ( 8.638326563840814399E-31, 0.000000000000000000, 1.000000000000000000 ) ) ;
#193124=( NAMED_UNIT ( * ) SI_UNIT ( $, .STERADIAN. ) SOLID_ANGLE_UNIT ( ) );
#193271=AXIS2_PLACEMENT_3D ( 'NONE', #91302, #10017, #174687 ) ;
#193398=CARTESIAN_POINT ( 'NONE',  ( -2.632325991586425218, 0.3920720250259056017, -0.1636427795756393855 ) ) ;
#193723=CARTESIAN_POINT ( 'NONE',  ( 2.679285714285720044, -0.4970443252110337551, -0.5000000000000004441 ) ) ;
#193810=CARTESIAN_POINT ( 'NONE',  ( -2.609770642201835855, -0.3830433331901521576, 0.000000000000000000 ) ) ;
#194006=ORIENTED_EDGE ( 'NONE', *, *, #63060, .F. ) ;
#194201=CARTESIAN_POINT ( 'NONE',  ( 1.850000000000000089, 4.013456704145457099E-20, 0.5999999999999969802 ) ) ;
#194299=EDGE_CURVE ( 'NONE', #167565, #138769, #127430, .T. ) ;
#194478=CARTESIAN_POINT ( 'NONE',  ( 1.600055350837883195, -1.204204895297025235, 1.480038727545127220 ) ) ;
#194519=VERTEX_POINT ( 'NONE', #157786 ) ;
#195105=CARTESIAN_POINT ( 'NONE',  ( -2.617062827300063343, -0.3852370113777853766, -0.1797355214283803959 ) ) ;
#195206=CARTESIAN_POINT ( 'NONE',  ( -1.559647396048210677, 1.374772708486763806, 1.500000000000001332 ) ) ;
#195457=CARTESIAN_POINT ( 'NONE',  ( 1.452583904633400591, 1.374772708486753370, 1.500000000000001332 ) ) ;
#195540=CARTESIAN_POINT ( 'NONE',  ( -2.680963302752293664, 0.4788041664877169534, -0.1016165050528608921 ) ) ;
#195568=EDGE_LOOP ( 'NONE', ( #63023, #122797, #45817, #28534, #119267, #81685, #116482, #172666, #5360, #122644, #2242 ) ) ;
#195835=CARTESIAN_POINT ( 'NONE',  ( 2.325000000000005063, 0.000000000000000000, -0.5000000000000004441 ) ) ;
#196138=CARTESIAN_POINT ( 'NONE',  ( -1.999999999999988010, 2.428614679364265457E-14, 0.5999999999999969802 ) ) ;
#196308=CIRCLE ( 'NONE', #161825, 2.000000000000000000 ) ;
#196339=ORIENTED_EDGE ( 'NONE', *, *, #87041, .F. ) ;
#196600=CIRCLE ( 'NONE', #65155, 0.09999999999999982514 ) ;
#196694=DIRECTION ( 'NONE',  ( 0.000000000000000000, 0.000000000000000000, -1.000000000000000000 ) ) ;
#196881=CARTESIAN_POINT ( 'NONE',  ( -1.812013678032658559, 0.3846686717400374933, 0.6718421233638942613 ) ) ;
#197356=EDGE_LOOP ( 'NONE', ( #150897, #27319, #125381, #96628 ) ) ;
#197649=CARTESIAN_POINT ( 'NONE',  ( -2.680963214763168789, 0.4786715097226356130, -0.1016399112248461689 ) ) ;
#197650=CARTESIAN_POINT ( 'NONE',  ( -5.249999999999987566, -0.9165151389911689872, 1.199999999999999734 ) ) ;
#197768=PRODUCT_CONTEXT ( 'NONE', #90556, 'mechanical' ) ;
#197875=ADVANCED_FACE ( 'NONE', ( #190517 ), #106138, .T. ) ;
#198575=CARTESIAN_POINT ( 'NONE',  ( -2.580963302752292243, 0.4788041664876945269, 0.000000000000000000 ) ) ;
#198788=FACE_OUTER_BOUND ( 'NONE', #13189, .T. ) ;
#198809=( LENGTH_UNIT ( ) NAMED_UNIT ( * ) SI_UNIT ( .MILLI., .METRE. ) );
#198888=DIRECTION ( 'NONE',  ( -1.000000000000000000, -3.451266460341927087E-31, 0.000000000000000000 ) ) ;
#198952=CARTESIAN_POINT ( 'NONE',  ( 1.651451222920913953, -0.8386022738108372954, 1.021479198850117287 ) ) ;
#199264=EDGE_CURVE ( 'NONE', #152613, #33663, #205342, .T. ) ;
#199484=CARTESIAN_POINT ( 'NONE',  ( 1.876272499184441500, -0.7121508056591638880, 0.8723429728170000175 ) ) ;
#199649=EDGE_CURVE ( 'NONE', #174147, #194519, #172833, .T. ) ;
#199667=ADVANCED_FACE ( 'NONE', ( #52194 ), #165943, .T. ) ;
#199736=EDGE_CURVE ( 'NONE', #126275, #162523, #177803, .T. ) ;
#199773=DIRECTION ( 'NONE',  ( -8.638326563840814399E-31, 0.000000000000000000, -1.000000000000000000 ) ) ;
#199964=DIRECTION ( 'NONE',  ( 8.638326563840814399E-31, -0.000000000000000000, 1.000000000000000000 ) ) ;
#200070=EDGE_CURVE ( 'NONE', #191630, #122458, #85224, .T. ) ;
#200407=AXIS2_PLACEMENT_3D ( 'NONE', #95216, #132002, #161266 ) ;
#200985=EDGE_CURVE ( 'NONE', #122127, #126275, #84957, .T. ) ;
#201438=ORIENTED_EDGE ( 'NONE', *, *, #150221, .F. ) ;
#201771=CYLINDRICAL_SURFACE ( 'NONE', #143924, 0.09999999999999982514 ) ;
#201896=EDGE_CURVE ( 'NONE', #15498, #106354, #196308, .T. ) ;
#202427=DIRECTION ( 'NONE',  ( 8.638326563840814399E-31, 0.000000000000000000, 1.000000000000000000 ) ) ;
#202961=DIRECTION ( 'NONE',  ( -1.000000000000000000, 0.000000000000000000, -8.638326563840826660E-31 ) ) ;
#203114=AXIS2_PLACEMENT_3D ( 'NONE', #190606, #27041, #61692 ) ;
#203221=VECTOR ( 'NONE', #151313, 1000.000000000000000 ) ;
#203718=CARTESIAN_POINT ( 'NONE',  ( -1.712858683735141163, -1.037413707456537715, 1.381497717048121299 ) ) ;
#203744=DIRECTION ( 'NONE',  ( 8.638326563840814399E-31, 0.000000000000000000, 1.000000000000000000 ) ) ;
#203806=B_SPLINE_CURVE_WITH_KNOTS ( 'NONE', 3,
 ( #103332, #20980, #72946, #186701, #40480, #74036, #206154, #123942 ),
 .UNSPECIFIED., .F., .F.,
 ( 4, 2, 2, 4 ),
 ( 0.0003130156513459781678, 0.0009018580307266956669, 0.001196279220417054579, 0.001490700410107413491 ),
 .UNSPECIFIED. ) ;
#204376=AXIS2_PLACEMENT_3D ( 'NONE', #3679, #23140, #202961 ) ;
#204623=FACE_OUTER_BOUND ( 'NONE', #14717, .T. ) ;
#205105=CARTESIAN_POINT ( 'NONE',  ( 1.850000000000000089, 6.384842951632563950E-31, -1.540743955509788682E-30 ) ) ;
#205177=AXIS2_PLACEMENT_3D ( 'NONE', #142391, #158611, #74158 ) ;
#205241=FACE_OUTER_BOUND ( 'NONE', #146336, .T. ) ;
#205342=LINE ( 'NONE', #120997, #57901 ) ;
#205407=CARTESIAN_POINT ( 'NONE',  ( 1.214306433183764966E-14, 2.428612866367529932E-14, 1.500000000000001332 ) ) ;
#205851=CARTESIAN_POINT ( 'NONE',  ( 2.680963302752393140, 0.4848410213525467527, -0.1005551520456971076 ) ) ;
#206079=FACE_OUTER_BOUND ( 'NONE', #154756, .T. ) ;
#206154=CARTESIAN_POINT ( 'NONE',  ( 2.000000000000012434, 0.09816220177719153783, 0.5999999999999995337 ) ) ;
#206433=ORIENTED_EDGE ( 'NONE', *, *, #64524, .F. ) ;
#206451=VECTOR ( 'NONE', #21806, 1000.000000000000000 ) ;
#206479=CARTESIAN_POINT ( 'NONE',  ( 1.580803134831910928, -0.9624764945123421844, 1.305310695360492712 ) ) ;
#206728=CYLINDRICAL_SURFACE ( 'NONE', #6278, 1.850000000000000089 ) ;
#206730=EDGE_LOOP ( 'NONE', ( #172450, #162693, #131368, #148021, #160821, #168999, #108200, #41322 ) ) ;
#206743=CARTESIAN_POINT ( 'NONE',  ( 1.532927541463139365, 1.041115454748538172, 1.384885517283059420 ) ) ;
#206860=DIRECTION ( 'NONE',  ( 8.638326563840814399E-31, -0.000000000000000000, 1.000000000000000000 ) ) ;
#207027=SURFACE_STYLE_USAGE ( .BOTH. , #70604 ) ;
#207059=EDGE_CURVE ( 'NONE', #52075, #15498, #77337, .T. ) ;
#207237=PRESENTATION_STYLE_ASSIGNMENT (( #157448 ) ) ;
#207245=ORIENTED_EDGE ( 'NONE', *, *, #6214, .T. ) ;
#207633=EDGE_CURVE ( 'NONE', #71186, #116404, #58450, .T. ) ;
#207640=CARTESIAN_POINT ( 'NONE',  ( -1.532410409194660650, 1.041802156240292376, 1.385306760018483407 ) ) ;
#207794=CARTESIAN_POINT ( 'NONE',  ( -2.679285714285713826, -0.4970443252110337551, -0.09999999999999592548 ) ) ;
#207803=CARTESIAN_POINT ( 'NONE',  ( 1.403658749385964244, 1.209764585679671933, 1.481909061747192391 ) ) ;
#207834=DIRECTION ( 'NONE',  ( 1.000000000000000000, 1.725633230170963762E-31, 8.638326563840814399E-31 ) ) ;
#207862=CARTESIAN_POINT ( 'NONE',  ( -1.651133652709660948, -0.8391591008036085597, 1.022755049771800984 ) ) ;
#207978=DIRECTION ( 'NONE',  ( -1.000000000000000000, -1.725633230170963762E-31, -8.638326563840814399E-31 ) ) ;
#208122=ORIENTED_EDGE ( 'NONE', *, *, #207059, .F. ) ;
#208163=EDGE_LOOP ( 'NONE', ( #182821, #88041 ) ) ;
#208294=CARTESIAN_POINT ( 'NONE',  ( -2.580963302752292243, -0.4788041664876945269, 0.000000000000000000 ) ) ;
#208746=CARTESIAN_POINT ( 'NONE',  ( -2.335486742378066527, -0.1025264918674536757, -0.4876558207452462712 ) ) ;
#208893=FACE_OUTER_BOUND ( 'NONE', #5322, .T. ) ;
#209417=AXIS2_PLACEMENT_3D ( 'NONE', #114650, #29072, #11736 ) ;
#209982=CYLINDRICAL_SURFACE ( 'NONE', #101294, 1.000000000000000222 ) ;
#210129=ORIENTED_EDGE ( 'NONE', *, *, #4927, .F. ) ;
#210441=CARTESIAN_POINT ( 'NONE',  ( 1.651133652709662947, 0.8391591008036050070, 1.022755049771794988 ) ) ;
#210701=ORIENTED_EDGE ( 'NONE', *, *, #62042, .F. ) ;
#210708=CARTESIAN_POINT ( 'NONE',  ( -2.679728069698085857, 0.4610709815545790957, -0.1059060488087512769 ) ) ;
#211085=CARTESIAN_POINT ( 'NONE',  ( -2.324999999999999289, 0.05106137233530610997, -0.5000000000000003331 ) ) ;
#211506=CARTESIAN_POINT ( 'NONE',  ( 1.715332513650478674, 0.7127186716553410850, 0.8729729531562329115 ) ) ;
#211678=CARTESIAN_POINT ( 'NONE',  ( 1.628336349302412112, 1.162346226930508264, 1.455206426644558571 ) ) ;
#211954=CARTESIAN_POINT ( 'NONE',  ( 0.000000000000000000, 0.000000000000000000, -0.09999999999999592548 ) ) ;
#212350=ORIENTED_EDGE ( 'NONE', *, *, #51590, .F. ) ;
#212431=CYLINDRICAL_SURFACE ( 'NONE', #149946, 0.09999999999999982514 ) ;
#212461=ORIENTED_EDGE ( 'NONE', *, *, #87337, .T. ) ;
#212504=COLOUR_RGB ( '', 0.40784314, 0.44705882, 0.49803922) ;
#212819=ORIENTED_EDGE ( 'NONE', *, *, #166683, .F. ) ;
#212928=ORIENTED_EDGE ( 'NONE', *, *, #30893, .T. ) ;
#213166=AXIS2_PLACEMENT_3D ( 'NONE', #105904, #155682, #188164 ) ;
#213499=CARTESIAN_POINT ( 'NONE',  ( 2.609770642201841184, -0.3830433331901555993, 0.000000000000000000 ) ) ;
#213719=CARTESIAN_POINT ( 'NONE',  ( 0.000000000000000000, 0.000000000000000000, 0.000000000000000000 ) ) ;
#213878=CARTESIAN_POINT ( 'NONE',  ( -2.665936209291942305, 0.4260822056534815938, -0.1252292841820018543 ) ) ;
#214163=CARTESIAN_POINT ( 'NONE',  ( 2.335486742378070968, 0.1025264918674481801, -0.4876558207452422189 ) ) ;
ENDSEC;
END-ISO-10303-21;
